ISO-10303-21;
HEADER;
/* Generated by software containing ST-Developer
 * from STEP Tools, Inc. (www.steptools.com) 
 */

FILE_DESCRIPTION(
/* description */ (''),
/* implementation_level */ '2;1');

FILE_NAME(
/* name */ '16_Port_Plug_1in_NPT.step',
/* time_stamp */ '2026-10-26T04:15:57-07:00',
/* author */ (''),
/* organization */ (''),
/* preprocessor_version */ 'ST-DEVELOPER v20.2',
/* originating_system */ 'Autodesk Translation Framework v15.15.0.0',
/* authorisation */ '');

FILE_SCHEMA (('AUTOMOTIVE_DESIGN { 1 0 10303 214 3 1 1 }'));
ENDSEC;

DATA;
#10=MECHANICAL_DESIGN_GEOMETRIC_PRESENTATION_REPRESENTATION('',(#465),#55737);
#383=CONICAL_SURFACE('',#29253,13.9397047631572,1.30899058790991);
#384=CONICAL_SURFACE('',#29256,16.15,1.04718484902493);
#385=CONICAL_SURFACE('',#29303,16.45,0.785398163397448);
#425=SHAPE_REPRESENTATION_RELATIONSHIP('SRR','None',#55834,#445);
#445=ADVANCED_BREP_SHAPE_REPRESENTATION('',(#485),#55730);
#465=STYLED_ITEM('',(#55977),#485);
#485=MANIFOLD_SOLID_BREP('Body1',#27234);
#571=B_SPLINE_SURFACE_WITH_KNOTS('',3,3,((#45582,#45583,#45584,#45585,#45586,
#45587),(#45588,#45589,#45590,#45591,#45592,#45593),(#45594,#45595,#45596,
#45597,#45598,#45599),(#45600,#45601,#45602,#45603,#45604,#45605)),
 .UNSPECIFIED.,.F.,.F.,.F.,(4,4),(4,1,1,4),(0.,1.),(0.217693875784178,0.975255008179982,
1.48029576311052,1.98533651804105),.UNSPECIFIED.);
#572=B_SPLINE_SURFACE_WITH_KNOTS('',3,3,((#45618,#45619,#45620,#45621,#45622,
#45623),(#45624,#45625,#45626,#45627,#45628,#45629),(#45630,#45631,#45632,
#45633,#45634,#45635),(#45636,#45637,#45638,#45639,#45640,#45641)),
 .UNSPECIFIED.,.F.,.F.,.F.,(4,4),(4,1,1,4),(0.,1.),(0.217693875784177,0.975255008179981,
1.48029576311052,1.98533651804105),.UNSPECIFIED.);
#573=B_SPLINE_SURFACE_WITH_KNOTS('',3,3,((#45648,#45649,#45650,#45651,#45652,
#45653),(#45654,#45655,#45656,#45657,#45658,#45659),(#45660,#45661,#45662,
#45663,#45664,#45665),(#45666,#45667,#45668,#45669,#45670,#45671)),
 .UNSPECIFIED.,.F.,.F.,.F.,(4,4),(4,1,1,4),(0.,1.),(0.217693875784177,0.975255008179981,
1.48029576311052,1.98533651804105),.UNSPECIFIED.);
#574=B_SPLINE_SURFACE_WITH_KNOTS('',3,3,((#45690,#45691,#45692,#45693,#45694,
#45695),(#45696,#45697,#45698,#45699,#45700,#45701),(#45702,#45703,#45704,
#45705,#45706,#45707),(#45708,#45709,#45710,#45711,#45712,#45713)),
 .UNSPECIFIED.,.F.,.F.,.F.,(4,4),(4,1,1,4),(0.,1.),(0.217693875784176,0.975255008179981,
1.48029576311052,1.98533651804105),.UNSPECIFIED.);
#575=B_SPLINE_SURFACE_WITH_KNOTS('',3,3,((#45720,#45721,#45722,#45723,#45724,
#45725),(#45726,#45727,#45728,#45729,#45730,#45731),(#45732,#45733,#45734,
#45735,#45736,#45737),(#45738,#45739,#45740,#45741,#45742,#45743)),
 .UNSPECIFIED.,.F.,.F.,.F.,(4,4),(4,1,1,4),(0.,1.),(0.217693875784177,0.975255008179981,
1.48029576311052,1.98533651804105),.UNSPECIFIED.);
#576=B_SPLINE_SURFACE_WITH_KNOTS('',3,3,((#45762,#45763,#45764,#45765,#45766,
#45767),(#45768,#45769,#45770,#45771,#45772,#45773),(#45774,#45775,#45776,
#45777,#45778,#45779),(#45780,#45781,#45782,#45783,#45784,#45785)),
 .UNSPECIFIED.,.F.,.F.,.F.,(4,4),(4,1,1,4),(0.,1.),(0.217693875784176,0.975255008179981,
1.48029576311052,1.98533651804105),.UNSPECIFIED.);
#1419=PLANE('',#29257);
#1420=PLANE('',#29258);
#1421=PLANE('',#29259);
#1422=PLANE('',#29260);
#1423=PLANE('',#29261);
#1424=PLANE('',#29262);
#1425=PLANE('',#29263);
#1426=PLANE('',#29264);
#1427=PLANE('',#29265);
#1428=PLANE('',#29266);
#1429=PLANE('',#29267);
#1430=PLANE('',#29268);
#1431=PLANE('',#29269);
#1432=PLANE('',#29270);
#1433=PLANE('',#29272);
#1434=PLANE('',#29273);
#1435=PLANE('',#29275);
#1436=PLANE('',#29276);
#1437=PLANE('',#29278);
#1438=PLANE('',#29279);
#1439=PLANE('',#29280);
#1440=PLANE('',#29281);
#1441=PLANE('',#29283);
#1442=PLANE('',#29285);
#1443=PLANE('',#29287);
#1444=PLANE('',#29288);
#1445=PLANE('',#29290);
#1446=PLANE('',#29292);
#1447=PLANE('',#29294);
#1448=PLANE('',#29296);
#1449=PLANE('',#29298);
#1450=PLANE('',#29301);
#3374=LINE('',#45434,#5745);
#3375=LINE('',#45472,#5746);
#3376=LINE('',#45489,#5747);
#3377=LINE('',#45517,#5748);
#3378=LINE('',#45521,#5749);
#3379=LINE('',#45549,#5750);
#3380=LINE('',#45553,#5751);
#3381=LINE('',#45581,#5752);
#3382=LINE('',#45615,#5753);
#3383=LINE('',#45616,#5754);
#3384=LINE('',#45617,#5755);
#3385=LINE('',#45681,#5756);
#3386=LINE('',#45682,#5757);
#3387=LINE('',#45683,#5758);
#3388=LINE('',#45687,#5759);
#3389=LINE('',#45688,#5760);
#3390=LINE('',#45689,#5761);
#3391=LINE('',#45753,#5762);
#3392=LINE('',#45754,#5763);
#3393=LINE('',#45755,#5764);
#3394=LINE('',#45759,#5765);
#3395=LINE('',#45760,#5766);
#3396=LINE('',#45761,#5767);
#3397=LINE('',#45795,#5768);
#3398=LINE('',#45796,#5769);
#3399=LINE('',#45797,#5770);
#3400=LINE('',#45800,#5771);
#3401=LINE('',#45803,#5772);
#3402=LINE('',#45806,#5773);
#3403=LINE('',#45807,#5774);
#3404=LINE('',#45810,#5775);
#3405=LINE('',#45814,#5776);
#3406=LINE('',#45815,#5777);
#3407=LINE('',#45818,#5778);
#3408=LINE('',#45822,#5779);
#3409=LINE('',#45823,#5780);
#3410=LINE('',#45826,#5781);
#3411=LINE('',#45828,#5782);
#3412=LINE('',#45829,#5783);
#3413=LINE('',#45832,#5784);
#3414=LINE('',#45834,#5785);
#3415=LINE('',#45835,#5786);
#3416=LINE('',#45838,#5787);
#3417=LINE('',#45845,#5788);
#3418=LINE('',#45866,#5789);
#3419=LINE('',#45868,#5790);
#5745=VECTOR('',#35178,13.9397047631572);
#5746=VECTOR('',#35183,16.15);
#5747=VECTOR('',#35188,10.);
#5748=VECTOR('',#35191,10.);
#5749=VECTOR('',#35194,10.);
#5750=VECTOR('',#35197,10.);
#5751=VECTOR('',#35200,10.);
#5752=VECTOR('',#35203,10.);
#5753=VECTOR('',#35206,10.);
#5754=VECTOR('',#35207,10.);
#5755=VECTOR('',#35208,10.);
#5756=VECTOR('',#35211,10.);
#5757=VECTOR('',#35212,10.);
#5758=VECTOR('',#35213,10.);
#5759=VECTOR('',#35216,10.);
#5760=VECTOR('',#35217,10.);
#5761=VECTOR('',#35218,10.);
#5762=VECTOR('',#35221,10.);
#5763=VECTOR('',#35222,10.);
#5764=VECTOR('',#35223,10.);
#5765=VECTOR('',#35226,10.);
#5766=VECTOR('',#35227,10.);
#5767=VECTOR('',#35228,10.);
#5768=VECTOR('',#35231,10.);
#5769=VECTOR('',#35232,10.);
#5770=VECTOR('',#35233,10.);
#5771=VECTOR('',#35236,10.);
#5772=VECTOR('',#35239,10.);
#5773=VECTOR('',#35242,10.);
#5774=VECTOR('',#35243,10.);
#5775=VECTOR('',#35246,10.);
#5776=VECTOR('',#35251,10.);
#5777=VECTOR('',#35252,10.);
#5778=VECTOR('',#35255,10.);
#5779=VECTOR('',#35260,10.);
#5780=VECTOR('',#35261,10.);
#5781=VECTOR('',#35264,10.);
#5782=VECTOR('',#35265,10.);
#5783=VECTOR('',#35266,10.);
#5784=VECTOR('',#35269,10.);
#5785=VECTOR('',#35270,10.);
#5786=VECTOR('',#35271,10.);
#5787=VECTOR('',#35274,10.);
#5788=VECTOR('',#35287,10.);
#5789=VECTOR('',#35322,16.45);
#5790=VECTOR('',#35325,16.7);
#6698=CYLINDRICAL_SURFACE('',#29305,16.7);
#7886=FACE_OUTER_BOUND('',#9555,.T.);
#7887=FACE_OUTER_BOUND('',#9556,.T.);
#7888=FACE_OUTER_BOUND('',#9557,.T.);
#7889=FACE_OUTER_BOUND('',#9558,.T.);
#7890=FACE_OUTER_BOUND('',#9559,.T.);
#7891=FACE_OUTER_BOUND('',#9560,.T.);
#7892=FACE_OUTER_BOUND('',#9561,.T.);
#7893=FACE_OUTER_BOUND('',#9562,.T.);
#7894=FACE_OUTER_BOUND('',#9563,.T.);
#7895=FACE_OUTER_BOUND('',#9564,.T.);
#7896=FACE_OUTER_BOUND('',#9565,.T.);
#7897=FACE_OUTER_BOUND('',#9566,.T.);
#7898=FACE_OUTER_BOUND('',#9567,.T.);
#7899=FACE_OUTER_BOUND('',#9568,.T.);
#7900=FACE_OUTER_BOUND('',#9569,.T.);
#7901=FACE_OUTER_BOUND('',#9570,.T.);
#7902=FACE_OUTER_BOUND('',#9571,.T.);
#7903=FACE_OUTER_BOUND('',#9572,.T.);
#7904=FACE_OUTER_BOUND('',#9573,.T.);
#7905=FACE_OUTER_BOUND('',#9574,.T.);
#7906=FACE_OUTER_BOUND('',#9575,.T.);
#7907=FACE_OUTER_BOUND('',#9576,.T.);
#7908=FACE_OUTER_BOUND('',#9577,.T.);
#7909=FACE_OUTER_BOUND('',#9578,.T.);
#7910=FACE_OUTER_BOUND('',#9579,.T.);
#7911=FACE_OUTER_BOUND('',#9580,.T.);
#7912=FACE_OUTER_BOUND('',#9581,.T.);
#7913=FACE_OUTER_BOUND('',#9582,.T.);
#7914=FACE_OUTER_BOUND('',#9583,.T.);
#7915=FACE_OUTER_BOUND('',#9584,.T.);
#7916=FACE_OUTER_BOUND('',#9585,.T.);
#7917=FACE_OUTER_BOUND('',#9586,.T.);
#7918=FACE_OUTER_BOUND('',#9587,.T.);
#7919=FACE_OUTER_BOUND('',#9588,.T.);
#7920=FACE_OUTER_BOUND('',#9589,.T.);
#7921=FACE_OUTER_BOUND('',#9590,.T.);
#7922=FACE_OUTER_BOUND('',#9591,.T.);
#7923=FACE_OUTER_BOUND('',#9592,.T.);
#7924=FACE_OUTER_BOUND('',#9593,.T.);
#7925=FACE_OUTER_BOUND('',#9594,.T.);
#7926=FACE_OUTER_BOUND('',#9595,.T.);
#7927=FACE_OUTER_BOUND('',#9596,.T.);
#9555=EDGE_LOOP('',(#23130,#23131,#23132,#23133));
#9556=EDGE_LOOP('',(#23134,#23135,#23136,#23137,#23138,#23139,#23140,#23141,
#23142,#23143));
#9557=EDGE_LOOP('',(#23144));
#9558=EDGE_LOOP('',(#23145,#23146,#23147));
#9559=EDGE_LOOP('',(#23148,#23149,#23150));
#9560=EDGE_LOOP('',(#23151,#23152,#23153));
#9561=EDGE_LOOP('',(#23154,#23155,#23156));
#9562=EDGE_LOOP('',(#23157,#23158,#23159));
#9563=EDGE_LOOP('',(#23160,#23161,#23162));
#9564=EDGE_LOOP('',(#23163,#23164,#23165,#23166));
#9565=EDGE_LOOP('',(#23167,#23168,#23169,#23170));
#9566=EDGE_LOOP('',(#23171,#23172,#23173,#23174));
#9567=EDGE_LOOP('',(#23175,#23176,#23177,#23178));
#9568=EDGE_LOOP('',(#23179,#23180,#23181,#23182));
#9569=EDGE_LOOP('',(#23183,#23184,#23185,#23186));
#9570=EDGE_LOOP('',(#23187,#23188,#23189,#23190));
#9571=EDGE_LOOP('',(#23191,#23192,#23193,#23194,#23195));
#9572=EDGE_LOOP('',(#23196,#23197,#23198,#23199));
#9573=EDGE_LOOP('',(#23200,#23201,#23202,#23203));
#9574=EDGE_LOOP('',(#23204,#23205,#23206,#23207));
#9575=EDGE_LOOP('',(#23208,#23209,#23210,#23211));
#9576=EDGE_LOOP('',(#23212,#23213,#23214,#23215));
#9577=EDGE_LOOP('',(#23216,#23217,#23218,#23219,#23220,#23221));
#9578=EDGE_LOOP('',(#23222,#23223,#23224,#23225));
#9579=EDGE_LOOP('',(#23226,#23227,#23228,#23229,#23230,#23231));
#9580=EDGE_LOOP('',(#23232,#23233,#23234,#23235));
#9581=EDGE_LOOP('',(#23236,#23237,#23238,#23239,#23240,#23241));
#9582=EDGE_LOOP('',(#23242,#23243,#23244,#23245,#23246,#23247));
#9583=EDGE_LOOP('',(#23248,#23249,#23250,#23251,#23252,#23253));
#9584=EDGE_LOOP('',(#23254,#23255,#23256,#23257));
#9585=EDGE_LOOP('',(#23258,#23259,#23260,#23261));
#9586=EDGE_LOOP('',(#23262,#23263,#23264,#23265));
#9587=EDGE_LOOP('',(#23266,#23267,#23268,#23269,#23270,#23271));
#9588=EDGE_LOOP('',(#23272,#23273));
#9589=EDGE_LOOP('',(#23274,#23275));
#9590=EDGE_LOOP('',(#23276,#23277));
#9591=EDGE_LOOP('',(#23278,#23279));
#9592=EDGE_LOOP('',(#23280,#23281));
#9593=EDGE_LOOP('',(#23282,#23283,#23284));
#9594=EDGE_LOOP('',(#23285));
#9595=EDGE_LOOP('',(#23286,#23287,#23288,#23289));
#9596=EDGE_LOOP('',(#23290,#23291,#23292,#23293,#23294,#23295,#23296,#23297,
#23298,#23299,#23300,#23301,#23302,#23303,#23304,#23305));
#10794=CIRCLE('',#29254,13.4732);
#10795=CIRCLE('',#29255,14.4062095263144);
#10796=CIRCLE('',#29271,16.7);
#10797=CIRCLE('',#29274,16.7);
#10798=CIRCLE('',#29277,16.7);
#10799=CIRCLE('',#29282,16.7);
#10800=CIRCLE('',#29284,16.7);
#10801=CIRCLE('',#29286,16.7);
#10802=CIRCLE('',#29289,16.7);
#10803=CIRCLE('',#29291,16.7);
#10804=CIRCLE('',#29293,16.7);
#10805=CIRCLE('',#29295,16.7);
#10806=CIRCLE('',#29297,16.7);
#10807=CIRCLE('',#29299,16.7);
#10808=CIRCLE('',#29300,16.7);
#10809=CIRCLE('',#29302,16.2);
#10810=CIRCLE('',#29304,16.7);
#11198=B_SPLINE_CURVE_WITH_KNOTS('',3,(#45439,#45440,#45441,#45442,#45443,
#45444),.UNSPECIFIED.,.F.,.F.,(4,1,1,4),(0.217693875784178,0.975255008179982,
1.48029576311052,1.98533651804105),.UNSPECIFIED.);
#11199=B_SPLINE_CURVE_WITH_KNOTS('',3,(#45446,#45447,#45448,#45449,#45450,
#45451),.UNSPECIFIED.,.F.,.F.,(4,1,1,4),(0.217693875784177,0.975255008179981,
1.48029576311052,1.98533651804105),.UNSPECIFIED.);
#11200=B_SPLINE_CURVE_WITH_KNOTS('',3,(#45453,#45454,#45455,#45456,#45457,
#45458),.UNSPECIFIED.,.F.,.F.,(4,1,1,4),(0.217693875784176,0.975255008179981,
1.48029576311052,1.98533651804105),.UNSPECIFIED.);
#11201=B_SPLINE_CURVE_WITH_KNOTS('',3,(#45460,#45461,#45462,#45463,#45464,
#45465),.UNSPECIFIED.,.F.,.F.,(4,1,1,4),(0.217693875784176,0.975255008179981,
1.48029576311052,1.98533651804105),.UNSPECIFIED.);
#11202=B_SPLINE_CURVE_WITH_KNOTS('',3,(#45467,#45468,#45469,#45470,#45471),
 .UNSPECIFIED.,.F.,.F.,(4,1,4),(1.10151519691261,1.48029576311052,1.98533651804105),
 .UNSPECIFIED.);
#11203=B_SPLINE_CURVE_WITH_KNOTS('',3,(#45474,#45475,#45476,#45477,#45478),
 .UNSPECIFIED.,.F.,.F.,(4,1,4),(0.217693875784177,0.975255008179981,1.10151519691261),
 .UNSPECIFIED.);
#11204=B_SPLINE_CURVE_WITH_KNOTS('',3,(#45479,#45480,#45481,#45482,#45483,
#45484),.UNSPECIFIED.,.F.,.F.,(4,1,1,4),(0.217693875784177,0.975255008179981,
1.48029576311052,1.98533651804105),.UNSPECIFIED.);
#11205=B_SPLINE_CURVE_WITH_KNOTS('',3,(#45490,#45491,#45492,#45493,#45494,
#45495),.UNSPECIFIED.,.F.,.F.,(4,2,4),(-0.0848441742917886,-0.0424181029814519,
0.),.UNSPECIFIED.);
#11206=B_SPLINE_CURVE_WITH_KNOTS('',3,(#45496,#45497,#45498,#45499,#45500,
#45501),.UNSPECIFIED.,.F.,.F.,(4,2,4),(-0.0848441721845653,-0.0424257383943444,
0.),.UNSPECIFIED.);
#11207=B_SPLINE_CURVE_WITH_KNOTS('',3,(#45504,#45505,#45506,#45507,#45508,
#45509),.UNSPECIFIED.,.F.,.F.,(4,2,4),(-0.0848441742849619,-0.0424181029793345,
0.),.UNSPECIFIED.);
#11208=B_SPLINE_CURVE_WITH_KNOTS('',3,(#45511,#45512,#45513,#45514,#45515,
#45516),.UNSPECIFIED.,.F.,.F.,(4,2,4),(-0.0848441721710981,-0.04242573838781,
0.),.UNSPECIFIED.);
#11209=B_SPLINE_CURVE_WITH_KNOTS('',3,(#45522,#45523,#45524,#45525,#45526,
#45527),.UNSPECIFIED.,.F.,.F.,(4,2,4),(-0.08484417429082,-0.0424181029808318,
0.),.UNSPECIFIED.);
#11210=B_SPLINE_CURVE_WITH_KNOTS('',3,(#45528,#45529,#45530,#45531,#45532,
#45533),.UNSPECIFIED.,.F.,.F.,(4,2,4),(-0.0848441721741252,-0.0424257383913701,
0.),.UNSPECIFIED.);
#11211=B_SPLINE_CURVE_WITH_KNOTS('',3,(#45536,#45537,#45538,#45539,#45540,
#45541),.UNSPECIFIED.,.F.,.F.,(4,2,4),(-0.0848441742890261,-0.0424181029805331,
0.),.UNSPECIFIED.);
#11212=B_SPLINE_CURVE_WITH_KNOTS('',3,(#45543,#45544,#45545,#45546,#45547,
#45548),.UNSPECIFIED.,.F.,.F.,(4,2,4),(-0.0848441721767493,-0.0424257383933299,
0.),.UNSPECIFIED.);
#11213=B_SPLINE_CURVE_WITH_KNOTS('',3,(#45554,#45555,#45556,#45557,#45558,
#45559),.UNSPECIFIED.,.F.,.F.,(4,2,4),(-0.0848441742833862,-0.0424181029791782,
0.),.UNSPECIFIED.);
#11214=B_SPLINE_CURVE_WITH_KNOTS('',3,(#45560,#45561,#45562,#45563,#45564,
#45565),.UNSPECIFIED.,.F.,.F.,(4,2,4),(-0.0848441721772216,-0.0424257383936094,
0.),.UNSPECIFIED.);
#11215=B_SPLINE_CURVE_WITH_KNOTS('',3,(#45568,#45569,#45570,#45571,#45572,
#45573),.UNSPECIFIED.,.F.,.F.,(4,2,4),(-0.0848441742900362,-0.0424181029807091,
0.),.UNSPECIFIED.);
#11216=B_SPLINE_CURVE_WITH_KNOTS('',3,(#45575,#45576,#45577,#45578,#45579,
#45580),.UNSPECIFIED.,.F.,.F.,(4,2,4),(-0.0848441721839697,-0.0424257383950013,
0.),.UNSPECIFIED.);
#11217=B_SPLINE_CURVE_WITH_KNOTS('',3,(#45606,#45607,#45608,#45609,#45610,
#45611),.UNSPECIFIED.,.F.,.F.,(4,1,1,4),(-1.98100236513816,-1.48029576311052,
-0.975255008179982,-0.222028028687133),.UNSPECIFIED.);
#11218=B_SPLINE_CURVE_WITH_KNOTS('',3,(#45642,#45643,#45644,#45645,#45646,
#45647),.UNSPECIFIED.,.F.,.F.,(4,1,1,4),(-1.98100236513816,-1.48029576311052,
-0.975255008179981,-0.222028028687133),.UNSPECIFIED.);
#11219=B_SPLINE_CURVE_WITH_KNOTS('',3,(#45672,#45673,#45674,#45675,#45676,
#45677),.UNSPECIFIED.,.F.,.F.,(4,1,1,4),(-1.98100236513816,-1.48029576311052,
-0.975255008179981,-0.222028028687133),.UNSPECIFIED.);
#11220=B_SPLINE_CURVE_WITH_KNOTS('',3,(#45714,#45715,#45716,#45717,#45718,
#45719),.UNSPECIFIED.,.F.,.F.,(4,1,1,4),(-1.98100236513816,-1.48029576311052,
-0.975255008179981,-0.222028028687132),.UNSPECIFIED.);
#11221=B_SPLINE_CURVE_WITH_KNOTS('',3,(#45744,#45745,#45746,#45747,#45748,
#45749),.UNSPECIFIED.,.F.,.F.,(4,1,1,4),(-1.98100236513816,-1.48029576311052,
-0.975255008179981,-0.222028028687132),.UNSPECIFIED.);
#11222=B_SPLINE_CURVE_WITH_KNOTS('',3,(#45786,#45787,#45788,#45789,#45790,
#45791),.UNSPECIFIED.,.F.,.F.,(4,1,1,4),(-1.98100236513816,-1.48029576311052,
-0.975255008179981,-0.222028028687132),.UNSPECIFIED.);
#13128=VERTEX_POINT('',#45431);
#13129=VERTEX_POINT('',#45433);
#13130=VERTEX_POINT('',#45437);
#13131=VERTEX_POINT('',#45438);
#13132=VERTEX_POINT('',#45445);
#13133=VERTEX_POINT('',#45452);
#13134=VERTEX_POINT('',#45459);
#13135=VERTEX_POINT('',#45466);
#13136=VERTEX_POINT('',#45473);
#13137=VERTEX_POINT('',#45487);
#13138=VERTEX_POINT('',#45488);
#13139=VERTEX_POINT('',#45503);
#13140=VERTEX_POINT('',#45510);
#13141=VERTEX_POINT('',#45519);
#13142=VERTEX_POINT('',#45520);
#13143=VERTEX_POINT('',#45535);
#13144=VERTEX_POINT('',#45542);
#13145=VERTEX_POINT('',#45551);
#13146=VERTEX_POINT('',#45552);
#13147=VERTEX_POINT('',#45567);
#13148=VERTEX_POINT('',#45574);
#13149=VERTEX_POINT('',#45613);
#13150=VERTEX_POINT('',#45614);
#13151=VERTEX_POINT('',#45679);
#13152=VERTEX_POINT('',#45680);
#13153=VERTEX_POINT('',#45685);
#13154=VERTEX_POINT('',#45686);
#13155=VERTEX_POINT('',#45751);
#13156=VERTEX_POINT('',#45752);
#13157=VERTEX_POINT('',#45757);
#13158=VERTEX_POINT('',#45758);
#13159=VERTEX_POINT('',#45793);
#13160=VERTEX_POINT('',#45794);
#13161=VERTEX_POINT('',#45799);
#13162=VERTEX_POINT('',#45801);
#13163=VERTEX_POINT('',#45805);
#13164=VERTEX_POINT('',#45809);
#13165=VERTEX_POINT('',#45813);
#13166=VERTEX_POINT('',#45817);
#13167=VERTEX_POINT('',#45821);
#13168=VERTEX_POINT('',#45825);
#13169=VERTEX_POINT('',#45827);
#13170=VERTEX_POINT('',#45831);
#13171=VERTEX_POINT('',#45833);
#13172=VERTEX_POINT('',#45837);
#13173=VERTEX_POINT('',#45857);
#13174=VERTEX_POINT('',#45861);
#13175=VERTEX_POINT('',#45864);
#16569=EDGE_CURVE('',#13128,#13128,#10794,.T.);
#16570=EDGE_CURVE('',#13128,#13129,#3374,.T.);
#16571=EDGE_CURVE('',#13129,#13129,#10795,.T.);
#16572=EDGE_CURVE('',#13130,#13131,#11198,.T.);
#16573=EDGE_CURVE('',#13132,#13130,#11199,.T.);
#16574=EDGE_CURVE('',#13133,#13132,#11200,.T.);
#16575=EDGE_CURVE('',#13134,#13133,#11201,.T.);
#16576=EDGE_CURVE('',#13135,#13134,#11202,.T.);
#16577=EDGE_CURVE('',#13135,#13129,#3375,.T.);
#16578=EDGE_CURVE('',#13136,#13135,#11203,.T.);
#16579=EDGE_CURVE('',#13131,#13136,#11204,.T.);
#16580=EDGE_CURVE('',#13137,#13138,#3376,.T.);
#16581=EDGE_CURVE('',#13134,#13137,#11205,.F.);
#16582=EDGE_CURVE('',#13138,#13134,#11206,.F.);
#16583=EDGE_CURVE('',#13133,#13139,#11207,.F.);
#16584=EDGE_CURVE('',#13140,#13133,#11208,.F.);
#16585=EDGE_CURVE('',#13139,#13140,#3377,.T.);
#16586=EDGE_CURVE('',#13141,#13142,#3378,.T.);
#16587=EDGE_CURVE('',#13136,#13141,#11209,.F.);
#16588=EDGE_CURVE('',#13142,#13136,#11210,.F.);
#16589=EDGE_CURVE('',#13132,#13143,#11211,.F.);
#16590=EDGE_CURVE('',#13144,#13132,#11212,.F.);
#16591=EDGE_CURVE('',#13143,#13144,#3379,.T.);
#16592=EDGE_CURVE('',#13145,#13146,#3380,.T.);
#16593=EDGE_CURVE('',#13131,#13145,#11213,.F.);
#16594=EDGE_CURVE('',#13146,#13131,#11214,.F.);
#16595=EDGE_CURVE('',#13130,#13147,#11215,.F.);
#16596=EDGE_CURVE('',#13148,#13130,#11216,.F.);
#16597=EDGE_CURVE('',#13147,#13148,#3381,.T.);
#16598=EDGE_CURVE('',#13145,#13148,#11217,.T.);
#16599=EDGE_CURVE('',#13149,#13150,#3382,.T.);
#16600=EDGE_CURVE('',#13150,#13147,#3383,.T.);
#16601=EDGE_CURVE('',#13148,#13149,#3384,.T.);
#16602=EDGE_CURVE('',#13147,#13144,#11218,.T.);
#16603=EDGE_CURVE('',#13141,#13146,#11219,.T.);
#16604=EDGE_CURVE('',#13151,#13152,#3385,.T.);
#16605=EDGE_CURVE('',#13152,#13145,#3386,.T.);
#16606=EDGE_CURVE('',#13146,#13151,#3387,.T.);
#16607=EDGE_CURVE('',#13153,#13154,#3388,.T.);
#16608=EDGE_CURVE('',#13154,#13143,#3389,.T.);
#16609=EDGE_CURVE('',#13144,#13153,#3390,.T.);
#16610=EDGE_CURVE('',#13143,#13140,#11220,.T.);
#16611=EDGE_CURVE('',#13137,#13142,#11221,.T.);
#16612=EDGE_CURVE('',#13155,#13156,#3391,.T.);
#16613=EDGE_CURVE('',#13156,#13141,#3392,.T.);
#16614=EDGE_CURVE('',#13142,#13155,#3393,.T.);
#16615=EDGE_CURVE('',#13157,#13158,#3394,.T.);
#16616=EDGE_CURVE('',#13158,#13139,#3395,.T.);
#16617=EDGE_CURVE('',#13140,#13157,#3396,.T.);
#16618=EDGE_CURVE('',#13139,#13138,#11222,.T.);
#16619=EDGE_CURVE('',#13159,#13160,#3397,.T.);
#16620=EDGE_CURVE('',#13160,#13137,#3398,.T.);
#16621=EDGE_CURVE('',#13138,#13159,#3399,.T.);
#16622=EDGE_CURVE('',#13161,#13151,#3400,.T.);
#16623=EDGE_CURVE('',#13161,#13162,#10796,.T.);
#16624=EDGE_CURVE('',#13152,#13162,#3401,.T.);
#16625=EDGE_CURVE('',#13156,#13163,#3402,.T.);
#16626=EDGE_CURVE('',#13161,#13163,#3403,.T.);
#16627=EDGE_CURVE('',#13164,#13155,#3404,.T.);
#16628=EDGE_CURVE('',#13164,#13163,#10797,.T.);
#16629=EDGE_CURVE('',#13160,#13165,#3405,.T.);
#16630=EDGE_CURVE('',#13164,#13165,#3406,.T.);
#16631=EDGE_CURVE('',#13166,#13159,#3407,.T.);
#16632=EDGE_CURVE('',#13166,#13165,#10798,.T.);
#16633=EDGE_CURVE('',#13158,#13167,#3408,.T.);
#16634=EDGE_CURVE('',#13166,#13167,#3409,.T.);
#16635=EDGE_CURVE('',#13154,#13168,#3410,.T.);
#16636=EDGE_CURVE('',#13169,#13168,#3411,.T.);
#16637=EDGE_CURVE('',#13169,#13157,#3412,.T.);
#16638=EDGE_CURVE('',#13150,#13170,#3413,.T.);
#16639=EDGE_CURVE('',#13171,#13170,#3414,.T.);
#16640=EDGE_CURVE('',#13171,#13153,#3415,.T.);
#16641=EDGE_CURVE('',#13172,#13149,#3416,.T.);
#16642=EDGE_CURVE('',#13172,#13170,#10799,.T.);
#16643=EDGE_CURVE('',#13171,#13168,#10800,.T.);
#16644=EDGE_CURVE('',#13169,#13167,#10801,.T.);
#16645=EDGE_CURVE('',#13172,#13162,#3417,.T.);
#16646=EDGE_CURVE('',#13167,#13166,#10802,.T.);
#16647=EDGE_CURVE('',#13168,#13169,#10803,.T.);
#16648=EDGE_CURVE('',#13170,#13171,#10804,.T.);
#16649=EDGE_CURVE('',#13162,#13172,#10805,.T.);
#16650=EDGE_CURVE('',#13163,#13161,#10806,.T.);
#16651=EDGE_CURVE('',#13165,#13173,#10807,.T.);
#16652=EDGE_CURVE('',#13173,#13164,#10808,.T.);
#16653=EDGE_CURVE('',#13174,#13174,#10809,.T.);
#16654=EDGE_CURVE('',#13175,#13175,#10810,.T.);
#16655=EDGE_CURVE('',#13175,#13174,#3418,.T.);
#16656=EDGE_CURVE('',#13173,#13175,#3419,.T.);
#23130=ORIENTED_EDGE('',*,*,#16569,.T.);
#23131=ORIENTED_EDGE('',*,*,#16570,.T.);
#23132=ORIENTED_EDGE('',*,*,#16571,.T.);
#23133=ORIENTED_EDGE('',*,*,#16570,.F.);
#23134=ORIENTED_EDGE('',*,*,#16572,.F.);
#23135=ORIENTED_EDGE('',*,*,#16573,.F.);
#23136=ORIENTED_EDGE('',*,*,#16574,.F.);
#23137=ORIENTED_EDGE('',*,*,#16575,.F.);
#23138=ORIENTED_EDGE('',*,*,#16576,.F.);
#23139=ORIENTED_EDGE('',*,*,#16577,.T.);
#23140=ORIENTED_EDGE('',*,*,#16571,.F.);
#23141=ORIENTED_EDGE('',*,*,#16577,.F.);
#23142=ORIENTED_EDGE('',*,*,#16578,.F.);
#23143=ORIENTED_EDGE('',*,*,#16579,.F.);
#23144=ORIENTED_EDGE('',*,*,#16569,.F.);
#23145=ORIENTED_EDGE('',*,*,#16580,.F.);
#23146=ORIENTED_EDGE('',*,*,#16581,.F.);
#23147=ORIENTED_EDGE('',*,*,#16582,.F.);
#23148=ORIENTED_EDGE('',*,*,#16583,.F.);
#23149=ORIENTED_EDGE('',*,*,#16584,.F.);
#23150=ORIENTED_EDGE('',*,*,#16585,.F.);
#23151=ORIENTED_EDGE('',*,*,#16586,.F.);
#23152=ORIENTED_EDGE('',*,*,#16587,.F.);
#23153=ORIENTED_EDGE('',*,*,#16588,.F.);
#23154=ORIENTED_EDGE('',*,*,#16589,.F.);
#23155=ORIENTED_EDGE('',*,*,#16590,.F.);
#23156=ORIENTED_EDGE('',*,*,#16591,.F.);
#23157=ORIENTED_EDGE('',*,*,#16592,.F.);
#23158=ORIENTED_EDGE('',*,*,#16593,.F.);
#23159=ORIENTED_EDGE('',*,*,#16594,.F.);
#23160=ORIENTED_EDGE('',*,*,#16595,.F.);
#23161=ORIENTED_EDGE('',*,*,#16596,.F.);
#23162=ORIENTED_EDGE('',*,*,#16597,.F.);
#23163=ORIENTED_EDGE('',*,*,#16593,.T.);
#23164=ORIENTED_EDGE('',*,*,#16598,.T.);
#23165=ORIENTED_EDGE('',*,*,#16596,.T.);
#23166=ORIENTED_EDGE('',*,*,#16572,.T.);
#23167=ORIENTED_EDGE('',*,*,#16599,.T.);
#23168=ORIENTED_EDGE('',*,*,#16600,.T.);
#23169=ORIENTED_EDGE('',*,*,#16597,.T.);
#23170=ORIENTED_EDGE('',*,*,#16601,.T.);
#23171=ORIENTED_EDGE('',*,*,#16595,.T.);
#23172=ORIENTED_EDGE('',*,*,#16602,.T.);
#23173=ORIENTED_EDGE('',*,*,#16590,.T.);
#23174=ORIENTED_EDGE('',*,*,#16573,.T.);
#23175=ORIENTED_EDGE('',*,*,#16587,.T.);
#23176=ORIENTED_EDGE('',*,*,#16603,.T.);
#23177=ORIENTED_EDGE('',*,*,#16594,.T.);
#23178=ORIENTED_EDGE('',*,*,#16579,.T.);
#23179=ORIENTED_EDGE('',*,*,#16604,.T.);
#23180=ORIENTED_EDGE('',*,*,#16605,.T.);
#23181=ORIENTED_EDGE('',*,*,#16592,.T.);
#23182=ORIENTED_EDGE('',*,*,#16606,.T.);
#23183=ORIENTED_EDGE('',*,*,#16607,.T.);
#23184=ORIENTED_EDGE('',*,*,#16608,.T.);
#23185=ORIENTED_EDGE('',*,*,#16591,.T.);
#23186=ORIENTED_EDGE('',*,*,#16609,.T.);
#23187=ORIENTED_EDGE('',*,*,#16589,.T.);
#23188=ORIENTED_EDGE('',*,*,#16610,.T.);
#23189=ORIENTED_EDGE('',*,*,#16584,.T.);
#23190=ORIENTED_EDGE('',*,*,#16574,.T.);
#23191=ORIENTED_EDGE('',*,*,#16581,.T.);
#23192=ORIENTED_EDGE('',*,*,#16611,.T.);
#23193=ORIENTED_EDGE('',*,*,#16588,.T.);
#23194=ORIENTED_EDGE('',*,*,#16578,.T.);
#23195=ORIENTED_EDGE('',*,*,#16576,.T.);
#23196=ORIENTED_EDGE('',*,*,#16612,.T.);
#23197=ORIENTED_EDGE('',*,*,#16613,.T.);
#23198=ORIENTED_EDGE('',*,*,#16586,.T.);
#23199=ORIENTED_EDGE('',*,*,#16614,.T.);
#23200=ORIENTED_EDGE('',*,*,#16615,.T.);
#23201=ORIENTED_EDGE('',*,*,#16616,.T.);
#23202=ORIENTED_EDGE('',*,*,#16585,.T.);
#23203=ORIENTED_EDGE('',*,*,#16617,.T.);
#23204=ORIENTED_EDGE('',*,*,#16583,.T.);
#23205=ORIENTED_EDGE('',*,*,#16618,.T.);
#23206=ORIENTED_EDGE('',*,*,#16582,.T.);
#23207=ORIENTED_EDGE('',*,*,#16575,.T.);
#23208=ORIENTED_EDGE('',*,*,#16619,.T.);
#23209=ORIENTED_EDGE('',*,*,#16620,.T.);
#23210=ORIENTED_EDGE('',*,*,#16580,.T.);
#23211=ORIENTED_EDGE('',*,*,#16621,.T.);
#23212=ORIENTED_EDGE('',*,*,#16604,.F.);
#23213=ORIENTED_EDGE('',*,*,#16622,.F.);
#23214=ORIENTED_EDGE('',*,*,#16623,.T.);
#23215=ORIENTED_EDGE('',*,*,#16624,.F.);
#23216=ORIENTED_EDGE('',*,*,#16606,.F.);
#23217=ORIENTED_EDGE('',*,*,#16603,.F.);
#23218=ORIENTED_EDGE('',*,*,#16613,.F.);
#23219=ORIENTED_EDGE('',*,*,#16625,.T.);
#23220=ORIENTED_EDGE('',*,*,#16626,.F.);
#23221=ORIENTED_EDGE('',*,*,#16622,.T.);
#23222=ORIENTED_EDGE('',*,*,#16612,.F.);
#23223=ORIENTED_EDGE('',*,*,#16627,.F.);
#23224=ORIENTED_EDGE('',*,*,#16628,.T.);
#23225=ORIENTED_EDGE('',*,*,#16625,.F.);
#23226=ORIENTED_EDGE('',*,*,#16614,.F.);
#23227=ORIENTED_EDGE('',*,*,#16611,.F.);
#23228=ORIENTED_EDGE('',*,*,#16620,.F.);
#23229=ORIENTED_EDGE('',*,*,#16629,.T.);
#23230=ORIENTED_EDGE('',*,*,#16630,.F.);
#23231=ORIENTED_EDGE('',*,*,#16627,.T.);
#23232=ORIENTED_EDGE('',*,*,#16619,.F.);
#23233=ORIENTED_EDGE('',*,*,#16631,.F.);
#23234=ORIENTED_EDGE('',*,*,#16632,.T.);
#23235=ORIENTED_EDGE('',*,*,#16629,.F.);
#23236=ORIENTED_EDGE('',*,*,#16621,.F.);
#23237=ORIENTED_EDGE('',*,*,#16618,.F.);
#23238=ORIENTED_EDGE('',*,*,#16616,.F.);
#23239=ORIENTED_EDGE('',*,*,#16633,.T.);
#23240=ORIENTED_EDGE('',*,*,#16634,.F.);
#23241=ORIENTED_EDGE('',*,*,#16631,.T.);
#23242=ORIENTED_EDGE('',*,*,#16608,.F.);
#23243=ORIENTED_EDGE('',*,*,#16635,.T.);
#23244=ORIENTED_EDGE('',*,*,#16636,.F.);
#23245=ORIENTED_EDGE('',*,*,#16637,.T.);
#23246=ORIENTED_EDGE('',*,*,#16617,.F.);
#23247=ORIENTED_EDGE('',*,*,#16610,.F.);
#23248=ORIENTED_EDGE('',*,*,#16600,.F.);
#23249=ORIENTED_EDGE('',*,*,#16638,.T.);
#23250=ORIENTED_EDGE('',*,*,#16639,.F.);
#23251=ORIENTED_EDGE('',*,*,#16640,.T.);
#23252=ORIENTED_EDGE('',*,*,#16609,.F.);
#23253=ORIENTED_EDGE('',*,*,#16602,.F.);
#23254=ORIENTED_EDGE('',*,*,#16599,.F.);
#23255=ORIENTED_EDGE('',*,*,#16641,.F.);
#23256=ORIENTED_EDGE('',*,*,#16642,.T.);
#23257=ORIENTED_EDGE('',*,*,#16638,.F.);
#23258=ORIENTED_EDGE('',*,*,#16607,.F.);
#23259=ORIENTED_EDGE('',*,*,#16640,.F.);
#23260=ORIENTED_EDGE('',*,*,#16643,.T.);
#23261=ORIENTED_EDGE('',*,*,#16635,.F.);
#23262=ORIENTED_EDGE('',*,*,#16615,.F.);
#23263=ORIENTED_EDGE('',*,*,#16637,.F.);
#23264=ORIENTED_EDGE('',*,*,#16644,.T.);
#23265=ORIENTED_EDGE('',*,*,#16633,.F.);
#23266=ORIENTED_EDGE('',*,*,#16605,.F.);
#23267=ORIENTED_EDGE('',*,*,#16624,.T.);
#23268=ORIENTED_EDGE('',*,*,#16645,.F.);
#23269=ORIENTED_EDGE('',*,*,#16641,.T.);
#23270=ORIENTED_EDGE('',*,*,#16601,.F.);
#23271=ORIENTED_EDGE('',*,*,#16598,.F.);
#23272=ORIENTED_EDGE('',*,*,#16634,.T.);
#23273=ORIENTED_EDGE('',*,*,#16646,.T.);
#23274=ORIENTED_EDGE('',*,*,#16636,.T.);
#23275=ORIENTED_EDGE('',*,*,#16647,.T.);
#23276=ORIENTED_EDGE('',*,*,#16639,.T.);
#23277=ORIENTED_EDGE('',*,*,#16648,.T.);
#23278=ORIENTED_EDGE('',*,*,#16645,.T.);
#23279=ORIENTED_EDGE('',*,*,#16649,.T.);
#23280=ORIENTED_EDGE('',*,*,#16626,.T.);
#23281=ORIENTED_EDGE('',*,*,#16650,.T.);
#23282=ORIENTED_EDGE('',*,*,#16630,.T.);
#23283=ORIENTED_EDGE('',*,*,#16651,.T.);
#23284=ORIENTED_EDGE('',*,*,#16652,.T.);
#23285=ORIENTED_EDGE('',*,*,#16653,.F.);
#23286=ORIENTED_EDGE('',*,*,#16654,.F.);
#23287=ORIENTED_EDGE('',*,*,#16655,.T.);
#23288=ORIENTED_EDGE('',*,*,#16653,.T.);
#23289=ORIENTED_EDGE('',*,*,#16655,.F.);
#23290=ORIENTED_EDGE('',*,*,#16648,.F.);
#23291=ORIENTED_EDGE('',*,*,#16642,.F.);
#23292=ORIENTED_EDGE('',*,*,#16649,.F.);
#23293=ORIENTED_EDGE('',*,*,#16623,.F.);
#23294=ORIENTED_EDGE('',*,*,#16650,.F.);
#23295=ORIENTED_EDGE('',*,*,#16628,.F.);
#23296=ORIENTED_EDGE('',*,*,#16652,.F.);
#23297=ORIENTED_EDGE('',*,*,#16656,.T.);
#23298=ORIENTED_EDGE('',*,*,#16654,.T.);
#23299=ORIENTED_EDGE('',*,*,#16656,.F.);
#23300=ORIENTED_EDGE('',*,*,#16651,.F.);
#23301=ORIENTED_EDGE('',*,*,#16632,.F.);
#23302=ORIENTED_EDGE('',*,*,#16646,.F.);
#23303=ORIENTED_EDGE('',*,*,#16644,.F.);
#23304=ORIENTED_EDGE('',*,*,#16647,.F.);
#23305=ORIENTED_EDGE('',*,*,#16643,.F.);
#26710=ADVANCED_FACE('',(#7886),#383,.T.);
#26711=ADVANCED_FACE('',(#7887),#384,.T.);
#26712=ADVANCED_FACE('',(#7888),#1419,.T.);
#26713=ADVANCED_FACE('',(#7889),#1420,.T.);
#26714=ADVANCED_FACE('',(#7890),#1421,.T.);
#26715=ADVANCED_FACE('',(#7891),#1422,.T.);
#26716=ADVANCED_FACE('',(#7892),#1423,.T.);
#26717=ADVANCED_FACE('',(#7893),#1424,.T.);
#26718=ADVANCED_FACE('',(#7894),#1425,.T.);
#26719=ADVANCED_FACE('',(#7895),#571,.T.);
#26720=ADVANCED_FACE('',(#7896),#1426,.T.);
#26721=ADVANCED_FACE('',(#7897),#572,.T.);
#26722=ADVANCED_FACE('',(#7898),#573,.T.);
#26723=ADVANCED_FACE('',(#7899),#1427,.T.);
#26724=ADVANCED_FACE('',(#7900),#1428,.T.);
#26725=ADVANCED_FACE('',(#7901),#574,.T.);
#26726=ADVANCED_FACE('',(#7902),#575,.T.);
#26727=ADVANCED_FACE('',(#7903),#1429,.T.);
#26728=ADVANCED_FACE('',(#7904),#1430,.T.);
#26729=ADVANCED_FACE('',(#7905),#576,.T.);
#26730=ADVANCED_FACE('',(#7906),#1431,.T.);
#26731=ADVANCED_FACE('',(#7907),#1432,.F.);
#26732=ADVANCED_FACE('',(#7908),#1433,.T.);
#26733=ADVANCED_FACE('',(#7909),#1434,.F.);
#26734=ADVANCED_FACE('',(#7910),#1435,.T.);
#26735=ADVANCED_FACE('',(#7911),#1436,.F.);
#26736=ADVANCED_FACE('',(#7912),#1437,.T.);
#26737=ADVANCED_FACE('',(#7913),#1438,.T.);
#26738=ADVANCED_FACE('',(#7914),#1439,.T.);
#26739=ADVANCED_FACE('',(#7915),#1440,.F.);
#26740=ADVANCED_FACE('',(#7916),#1441,.F.);
#26741=ADVANCED_FACE('',(#7917),#1442,.F.);
#26742=ADVANCED_FACE('',(#7918),#1443,.T.);
#26743=ADVANCED_FACE('',(#7919),#1444,.T.);
#26744=ADVANCED_FACE('',(#7920),#1445,.T.);
#26745=ADVANCED_FACE('',(#7921),#1446,.T.);
#26746=ADVANCED_FACE('',(#7922),#1447,.T.);
#26747=ADVANCED_FACE('',(#7923),#1448,.T.);
#26748=ADVANCED_FACE('',(#7924),#1449,.T.);
#26749=ADVANCED_FACE('',(#7925),#1450,.T.);
#26750=ADVANCED_FACE('',(#7926),#385,.T.);
#26751=ADVANCED_FACE('',(#7927),#6698,.T.);
#27234=CLOSED_SHELL('',(#26710,#26711,#26712,#26713,#26714,#26715,#26716,
#26717,#26718,#26719,#26720,#26721,#26722,#26723,#26724,#26725,#26726,#26727,
#26728,#26729,#26730,#26731,#26732,#26733,#26734,#26735,#26736,#26737,#26738,
#26739,#26740,#26741,#26742,#26743,#26744,#26745,#26746,#26747,#26748,#26749,
#26750,#26751));
#29252=AXIS2_PLACEMENT_3D('',#45429,#35172,#35173);
#29253=AXIS2_PLACEMENT_3D('',#45430,#35174,#35175);
#29254=AXIS2_PLACEMENT_3D('',#45432,#35176,#35177);
#29255=AXIS2_PLACEMENT_3D('',#45435,#35179,#35180);
#29256=AXIS2_PLACEMENT_3D('',#45436,#35181,#35182);
#29257=AXIS2_PLACEMENT_3D('',#45485,#35184,#35185);
#29258=AXIS2_PLACEMENT_3D('',#45486,#35186,#35187);
#29259=AXIS2_PLACEMENT_3D('',#45502,#35189,#35190);
#29260=AXIS2_PLACEMENT_3D('',#45518,#35192,#35193);
#29261=AXIS2_PLACEMENT_3D('',#45534,#35195,#35196);
#29262=AXIS2_PLACEMENT_3D('',#45550,#35198,#35199);
#29263=AXIS2_PLACEMENT_3D('',#45566,#35201,#35202);
#29264=AXIS2_PLACEMENT_3D('',#45612,#35204,#35205);
#29265=AXIS2_PLACEMENT_3D('',#45678,#35209,#35210);
#29266=AXIS2_PLACEMENT_3D('',#45684,#35214,#35215);
#29267=AXIS2_PLACEMENT_3D('',#45750,#35219,#35220);
#29268=AXIS2_PLACEMENT_3D('',#45756,#35224,#35225);
#29269=AXIS2_PLACEMENT_3D('',#45792,#35229,#35230);
#29270=AXIS2_PLACEMENT_3D('',#45798,#35234,#35235);
#29271=AXIS2_PLACEMENT_3D('',#45802,#35237,#35238);
#29272=AXIS2_PLACEMENT_3D('',#45804,#35240,#35241);
#29273=AXIS2_PLACEMENT_3D('',#45808,#35244,#35245);
#29274=AXIS2_PLACEMENT_3D('',#45811,#35247,#35248);
#29275=AXIS2_PLACEMENT_3D('',#45812,#35249,#35250);
#29276=AXIS2_PLACEMENT_3D('',#45816,#35253,#35254);
#29277=AXIS2_PLACEMENT_3D('',#45819,#35256,#35257);
#29278=AXIS2_PLACEMENT_3D('',#45820,#35258,#35259);
#29279=AXIS2_PLACEMENT_3D('',#45824,#35262,#35263);
#29280=AXIS2_PLACEMENT_3D('',#45830,#35267,#35268);
#29281=AXIS2_PLACEMENT_3D('',#45836,#35272,#35273);
#29282=AXIS2_PLACEMENT_3D('',#45839,#35275,#35276);
#29283=AXIS2_PLACEMENT_3D('',#45840,#35277,#35278);
#29284=AXIS2_PLACEMENT_3D('',#45841,#35279,#35280);
#29285=AXIS2_PLACEMENT_3D('',#45842,#35281,#35282);
#29286=AXIS2_PLACEMENT_3D('',#45843,#35283,#35284);
#29287=AXIS2_PLACEMENT_3D('',#45844,#35285,#35286);
#29288=AXIS2_PLACEMENT_3D('',#45846,#35288,#35289);
#29289=AXIS2_PLACEMENT_3D('',#45847,#35290,#35291);
#29290=AXIS2_PLACEMENT_3D('',#45848,#35292,#35293);
#29291=AXIS2_PLACEMENT_3D('',#45849,#35294,#35295);
#29292=AXIS2_PLACEMENT_3D('',#45850,#35296,#35297);
#29293=AXIS2_PLACEMENT_3D('',#45851,#35298,#35299);
#29294=AXIS2_PLACEMENT_3D('',#45852,#35300,#35301);
#29295=AXIS2_PLACEMENT_3D('',#45853,#35302,#35303);
#29296=AXIS2_PLACEMENT_3D('',#45854,#35304,#35305);
#29297=AXIS2_PLACEMENT_3D('',#45855,#35306,#35307);
#29298=AXIS2_PLACEMENT_3D('',#45856,#35308,#35309);
#29299=AXIS2_PLACEMENT_3D('',#45858,#35310,#35311);
#29300=AXIS2_PLACEMENT_3D('',#45859,#35312,#35313);
#29301=AXIS2_PLACEMENT_3D('',#45860,#35314,#35315);
#29302=AXIS2_PLACEMENT_3D('',#45862,#35316,#35317);
#29303=AXIS2_PLACEMENT_3D('',#45863,#35318,#35319);
#29304=AXIS2_PLACEMENT_3D('',#45865,#35320,#35321);
#29305=AXIS2_PLACEMENT_3D('',#45867,#35323,#35324);
#35172=DIRECTION('axis',(0.,0.,1.));
#35173=DIRECTION('refdir',(1.,0.,0.));
#35174=DIRECTION('center_axis',(-1.,0.,-3.52842604891459E-15));
#35175=DIRECTION('ref_axis',(0.,1.,3.1640767656135E-17));
#35176=DIRECTION('center_axis',(-1.,0.,0.));
#35177=DIRECTION('ref_axis',(0.,1.,0.));
#35178=DIRECTION('',(-0.258825179775134,-0.965924182487616,-1.06209968489537E-15));
#35179=DIRECTION('center_axis',(1.,0.,0.));
#35180=DIRECTION('ref_axis',(0.,1.,6.12323399573677E-17));
#35181=DIRECTION('center_axis',(-1.,0.,0.));
#35182=DIRECTION('ref_axis',(0.,1.,0.));
#35183=DIRECTION('',(0.500011000363013,0.866019052628739,1.06056746080241E-16));
#35184=DIRECTION('center_axis',(1.,0.,0.));
#35185=DIRECTION('ref_axis',(0.,0.,-1.));
#35186=DIRECTION('center_axis',(0.369852508213401,-0.804615959092168,0.464545240576681));
#35187=DIRECTION('ref_axis',(0.782331963393017,0.,-0.622861701386133));
#35188=DIRECTION('',(0.,0.500000000000002,0.866025403784438));
#35189=DIRECTION('center_axis',(0.369852508213402,4.69866669311145E-13,
0.929090481152538));
#35190=DIRECTION('ref_axis',(0.929090481152538,0.,-0.369852508213402));
#35191=DIRECTION('',(0.,1.,2.56395024851141E-15));
#35192=DIRECTION('center_axis',(0.369852508213404,-0.804615959092644,-0.464545240575855));
#35193=DIRECTION('ref_axis',(-0.782331963392475,0.,-0.622861701386813));
#35194=DIRECTION('',(-2.56395024851143E-15,-0.499999999999999,0.866025403784439));
#35195=DIRECTION('center_axis',(0.369852508213404,0.804615959092643,0.464545240575856));
#35196=DIRECTION('ref_axis',(0.782331963392475,0.,-0.622861701386812));
#35197=DIRECTION('',(1.28197512425571E-15,0.499999999999999,-0.866025403784439));
#35198=DIRECTION('center_axis',(0.3698525082134,-4.77010775225235E-13,-0.929090481152539));
#35199=DIRECTION('ref_axis',(-0.929090481152539,0.,-0.3698525082134));
#35200=DIRECTION('',(-1.28197512425571E-15,-1.,2.56395024851142E-15));
#35201=DIRECTION('center_axis',(0.369852508213402,0.80461595909217,-0.464545240576677));
#35202=DIRECTION('ref_axis',(-0.782331963393014,0.,-0.622861701386136));
#35203=DIRECTION('',(-2.56395024851142E-15,-0.499999999999997,-0.86602540378444));
#35204=DIRECTION('center_axis',(0.,0.86602540378444,-0.499999999999997));
#35205=DIRECTION('ref_axis',(0.,0.499999999999997,0.86602540378444));
#35206=DIRECTION('',(0.,0.499999999999997,0.86602540378444));
#35207=DIRECTION('',(1.,0.,0.));
#35208=DIRECTION('',(-1.,0.,0.));
#35209=DIRECTION('center_axis',(0.,-2.56395024851142E-15,-1.));
#35210=DIRECTION('ref_axis',(-1.,0.,0.));
#35211=DIRECTION('',(0.,1.,-2.56395024851142E-15));
#35212=DIRECTION('',(1.,0.,0.));
#35213=DIRECTION('',(-1.,0.,0.));
#35214=DIRECTION('center_axis',(0.,0.866025403784439,0.499999999999999));
#35215=DIRECTION('ref_axis',(0.,-0.499999999999999,0.866025403784439));
#35216=DIRECTION('',(0.,-0.499999999999999,0.866025403784439));
#35217=DIRECTION('',(1.,0.,0.));
#35218=DIRECTION('',(-1.,0.,0.));
#35219=DIRECTION('center_axis',(0.,-0.866025403784439,-0.499999999999999));
#35220=DIRECTION('ref_axis',(0.,0.499999999999999,-0.866025403784439));
#35221=DIRECTION('',(0.,0.499999999999999,-0.866025403784439));
#35222=DIRECTION('',(1.,0.,0.));
#35223=DIRECTION('',(-1.,0.,0.));
#35224=DIRECTION('center_axis',(0.,-2.56395024851141E-15,1.));
#35225=DIRECTION('ref_axis',(1.,0.,0.));
#35226=DIRECTION('',(0.,-1.,-2.56395024851141E-15));
#35227=DIRECTION('',(1.,0.,0.));
#35228=DIRECTION('',(-1.,0.,0.));
#35229=DIRECTION('center_axis',(0.,-0.866025403784438,0.500000000000002));
#35230=DIRECTION('ref_axis',(1.,0.,0.));
#35231=DIRECTION('',(0.,-0.500000000000002,-0.866025403784438));
#35232=DIRECTION('',(1.,0.,0.));
#35233=DIRECTION('',(-1.,0.,0.));
#35234=DIRECTION('center_axis',(1.,0.,0.));
#35235=DIRECTION('ref_axis',(0.,0.,-1.));
#35236=DIRECTION('',(0.,0.866025403784439,-0.5));
#35237=DIRECTION('center_axis',(1.,0.,0.));
#35238=DIRECTION('ref_axis',(0.,0.,-1.));
#35239=DIRECTION('',(0.,0.866025403784439,0.5));
#35240=DIRECTION('center_axis',(0.,-0.5,-0.866025403784439));
#35241=DIRECTION('ref_axis',(0.,0.866025403784439,-0.5));
#35242=DIRECTION('',(0.,0.866025403784439,-0.5));
#35243=DIRECTION('',(0.,-0.866025403784439,0.5));
#35244=DIRECTION('center_axis',(1.,0.,0.));
#35245=DIRECTION('ref_axis',(0.,0.,-1.));
#35246=DIRECTION('',(0.,1.28197512425571E-16,-1.));
#35247=DIRECTION('center_axis',(1.,0.,0.));
#35248=DIRECTION('ref_axis',(0.,0.,-1.));
#35249=DIRECTION('center_axis',(0.,-1.,-1.28197512425571E-16));
#35250=DIRECTION('ref_axis',(0.,1.28197512425571E-16,-1.));
#35251=DIRECTION('',(0.,1.28197512425571E-16,-1.));
#35252=DIRECTION('',(0.,-1.28197512425571E-16,1.));
#35253=DIRECTION('center_axis',(1.,0.,0.));
#35254=DIRECTION('ref_axis',(0.,0.,-1.));
#35255=DIRECTION('',(0.,-0.866025403784439,-0.5));
#35256=DIRECTION('center_axis',(1.,0.,0.));
#35257=DIRECTION('ref_axis',(0.,0.,-1.));
#35258=DIRECTION('center_axis',(0.,-0.5,0.866025403784439));
#35259=DIRECTION('ref_axis',(0.,-0.866025403784439,-0.5));
#35260=DIRECTION('',(0.,-0.866025403784439,-0.5));
#35261=DIRECTION('',(0.,0.866025403784439,0.5));
#35262=DIRECTION('center_axis',(0.,0.5,0.866025403784439));
#35263=DIRECTION('ref_axis',(0.,-0.866025403784439,0.5));
#35264=DIRECTION('',(0.,-0.866025403784439,0.5));
#35265=DIRECTION('',(0.,0.866025403784439,-0.5));
#35266=DIRECTION('',(0.,-0.866025403784439,0.5));
#35267=DIRECTION('center_axis',(0.,1.,-3.84592537276713E-16));
#35268=DIRECTION('ref_axis',(0.,3.84592537276713E-16,1.));
#35269=DIRECTION('',(0.,3.84592537276713E-16,1.));
#35270=DIRECTION('',(0.,-3.84592537276713E-16,-1.));
#35271=DIRECTION('',(0.,3.84592537276713E-16,1.));
#35272=DIRECTION('center_axis',(1.,0.,0.));
#35273=DIRECTION('ref_axis',(0.,0.,-1.));
#35274=DIRECTION('',(0.,0.866025403784439,0.5));
#35275=DIRECTION('center_axis',(1.,0.,0.));
#35276=DIRECTION('ref_axis',(0.,0.,-1.));
#35277=DIRECTION('center_axis',(1.,0.,0.));
#35278=DIRECTION('ref_axis',(0.,0.,-1.));
#35279=DIRECTION('center_axis',(1.,0.,0.));
#35280=DIRECTION('ref_axis',(0.,0.,-1.));
#35281=DIRECTION('center_axis',(1.,0.,0.));
#35282=DIRECTION('ref_axis',(0.,0.,-1.));
#35283=DIRECTION('center_axis',(1.,0.,0.));
#35284=DIRECTION('ref_axis',(0.,0.,-1.));
#35285=DIRECTION('center_axis',(0.,0.5,-0.866025403784439));
#35286=DIRECTION('ref_axis',(0.,0.866025403784439,0.5));
#35287=DIRECTION('',(0.,-0.866025403784439,-0.5));
#35288=DIRECTION('center_axis',(1.,0.,0.));
#35289=DIRECTION('ref_axis',(0.,0.,-1.));
#35290=DIRECTION('center_axis',(1.,0.,0.));
#35291=DIRECTION('ref_axis',(0.,0.,-1.));
#35292=DIRECTION('center_axis',(1.,0.,0.));
#35293=DIRECTION('ref_axis',(0.,0.,-1.));
#35294=DIRECTION('center_axis',(1.,0.,0.));
#35295=DIRECTION('ref_axis',(0.,0.,-1.));
#35296=DIRECTION('center_axis',(1.,0.,0.));
#35297=DIRECTION('ref_axis',(0.,0.,-1.));
#35298=DIRECTION('center_axis',(1.,0.,0.));
#35299=DIRECTION('ref_axis',(0.,0.,-1.));
#35300=DIRECTION('center_axis',(1.,0.,0.));
#35301=DIRECTION('ref_axis',(0.,0.,-1.));
#35302=DIRECTION('center_axis',(1.,0.,0.));
#35303=DIRECTION('ref_axis',(0.,0.,-1.));
#35304=DIRECTION('center_axis',(1.,0.,0.));
#35305=DIRECTION('ref_axis',(0.,0.,-1.));
#35306=DIRECTION('center_axis',(1.,0.,0.));
#35307=DIRECTION('ref_axis',(0.,0.,-1.));
#35308=DIRECTION('center_axis',(1.,0.,0.));
#35309=DIRECTION('ref_axis',(0.,0.,-1.));
#35310=DIRECTION('center_axis',(1.,0.,0.));
#35311=DIRECTION('ref_axis',(0.,0.,-1.));
#35312=DIRECTION('center_axis',(1.,0.,0.));
#35313=DIRECTION('ref_axis',(0.,0.,-1.));
#35314=DIRECTION('center_axis',(-1.,0.,0.));
#35315=DIRECTION('ref_axis',(0.,0.,1.));
#35316=DIRECTION('center_axis',(1.,0.,0.));
#35317=DIRECTION('ref_axis',(0.,0.,-1.));
#35318=DIRECTION('center_axis',(1.,0.,0.));
#35319=DIRECTION('ref_axis',(0.,1.,0.));
#35320=DIRECTION('center_axis',(1.,0.,0.));
#35321=DIRECTION('ref_axis',(0.,0.,-1.));
#35322=DIRECTION('',(-0.707106781186548,0.707106781186548,8.65956056235493E-17));
#35323=DIRECTION('center_axis',(1.,0.,0.));
#35324=DIRECTION('ref_axis',(0.,1.,0.));
#35325=DIRECTION('',(-1.,0.,0.));
#45429=CARTESIAN_POINT('',(0.,0.,0.));
#45430=CARTESIAN_POINT('Origin',(9.87499724990925,0.,-4.41062959606175E-16));
#45431=CARTESIAN_POINT('',(10.,-13.4732,1.64999112542721E-15));
#45432=CARTESIAN_POINT('Origin',(10.,0.,0.));
#45433=CARTESIAN_POINT('',(9.74999449981849,-14.4062095263144,-3.5285036768494E-15));
#45434=CARTESIAN_POINT('',(9.87499724990925,-13.9397047631572,-2.58924740113831E-15));
#45435=CARTESIAN_POINT('Origin',(9.74999449981849,0.,-8.8212591921235E-16));
#45436=CARTESIAN_POINT('Origin',(8.7431870669746,0.,0.));
#45437=CARTESIAN_POINT('',(8.36752131451236,14.5497923702765,-8.40032654163231));
#45438=CARTESIAN_POINT('',(8.36752131451235,-3.33066907387547E-15,-16.8006530832646));
#45439=CARTESIAN_POINT('Ctrl Pts',(8.36752131451236,14.5497923702765,-8.40032654163231));
#45440=CARTESIAN_POINT('Ctrl Pts',(9.15318176943128,12.1845393672071,-9.77553709986417));
#45441=CARTESIAN_POINT('Ctrl Pts',(9.79023847218445,8.88417527786995,-11.6941257536935));
#45442=CARTESIAN_POINT('Ctrl Pts',(9.57244918857082,4.39048143018587,-14.2836892688202));
#45443=CARTESIAN_POINT('Ctrl Pts',(8.89129495112497,1.58239585367736,-15.8934771446516));
#45444=CARTESIAN_POINT('Ctrl Pts',(8.36752131451235,-8.88178419700125E-15,
-16.8006530832646));
#45445=CARTESIAN_POINT('',(8.36752131451236,14.5497923702765,8.4003265416323));
#45446=CARTESIAN_POINT('Ctrl Pts',(8.36752131451236,14.5497923702765,8.4003265416323));
#45447=CARTESIAN_POINT('Ctrl Pts',(9.15318176943128,14.5581331477232,5.66435207548085));
#45448=CARTESIAN_POINT('Ctrl Pts',(9.79054641267288,14.5694951319271,1.84651364397653));
#45449=CARTESIAN_POINT('Ctrl Pts',(9.57257984044265,14.565278525504,-3.33951930676775));
#45450=CARTESIAN_POINT('Ctrl Pts',(8.89129495112498,14.5553528885743,-6.57634356419801));
#45451=CARTESIAN_POINT('Ctrl Pts',(8.36752131451236,14.5497923702765,-8.40032654163231));
#45452=CARTESIAN_POINT('',(8.36752131451236,5.55111512312578E-16,16.8006530832646));
#45453=CARTESIAN_POINT('Ctrl Pts',(8.36752131451236,-5.55111512312578E-16,
16.8006530832646));
#45454=CARTESIAN_POINT('Ctrl Pts',(9.15318176943128,2.37359378051606,15.439889175345));
#45455=CARTESIAN_POINT('Ctrl Pts',(9.79023847218445,5.68532233881341,13.5409843591558));
#45456=CARTESIAN_POINT('Ctrl Pts',(9.57244918857082,10.1747970514685,10.9441130877949));
#45457=CARTESIAN_POINT('Ctrl Pts',(8.89129495112497,12.9729570348969,9.31713358045354));
#45458=CARTESIAN_POINT('Ctrl Pts',(8.36752131451235,14.5497923702765,8.4003265416323));
#45459=CARTESIAN_POINT('',(8.36752131451235,-14.5497923702765,8.4003265416323));
#45460=CARTESIAN_POINT('Ctrl Pts',(8.36752131451235,-14.5497923702765,8.4003265416323));
#45461=CARTESIAN_POINT('Ctrl Pts',(9.15318176943129,-12.1845393672071,9.77553709986416));
#45462=CARTESIAN_POINT('Ctrl Pts',(9.79023847218445,-8.88417527786995,11.6941257536935));
#45463=CARTESIAN_POINT('Ctrl Pts',(9.57244918857083,-4.39048143018589,14.2836892688202));
#45464=CARTESIAN_POINT('Ctrl Pts',(8.89129495112497,-1.58239585367737,15.8934771446515));
#45465=CARTESIAN_POINT('Ctrl Pts',(8.36752131451235,4.44089209850063E-15,
16.8006530832646));
#45466=CARTESIAN_POINT('',(9.65699525572486,-14.5669896065098,-0.00095436007870299));
#45467=CARTESIAN_POINT('Ctrl Pts',(9.65699525572486,-14.5669896065098,-0.000954360078702712));
#45468=CARTESIAN_POINT('Ctrl Pts',(9.65729513939778,-14.5669682027371,1.12120526983947));
#45469=CARTESIAN_POINT('Ctrl Pts',(9.48741922927794,-14.5640378208878,3.74412233894653));
#45470=CARTESIAN_POINT('Ctrl Pts',(8.89129495112497,-14.5553528885743,6.576343564198));
#45471=CARTESIAN_POINT('Ctrl Pts',(8.36752131451236,-14.5497923702765,8.4003265416323));
#45472=CARTESIAN_POINT('',(8.7431870669746,-16.15,-1.97780458062298E-15));
#45473=CARTESIAN_POINT('',(8.36752131451236,-14.5497923702765,-8.4003265416323));
#45474=CARTESIAN_POINT('Ctrl Pts',(8.36752131451236,-14.5497923702765,-8.4003265416323));
#45475=CARTESIAN_POINT('Ctrl Pts',(9.15318176943128,-14.5581331477232,-5.66435207548086));
#45476=CARTESIAN_POINT('Ctrl Pts',(9.5993370197004,-14.5660865366659,-2.99186517342783));
#45477=CARTESIAN_POINT('Ctrl Pts',(9.65689529450055,-14.5669967411007,-0.375007570051427));
#45478=CARTESIAN_POINT('Ctrl Pts',(9.65699525572486,-14.5669896065098,-0.000954360078702712));
#45479=CARTESIAN_POINT('Ctrl Pts',(8.36752131451236,-3.33066907387547E-15,
-16.8006530832646));
#45480=CARTESIAN_POINT('Ctrl Pts',(9.15318176943128,-2.37359378051606,-15.439889175345));
#45481=CARTESIAN_POINT('Ctrl Pts',(9.79023847218444,-5.6853223388134,-13.5409843591558));
#45482=CARTESIAN_POINT('Ctrl Pts',(9.57244918857082,-10.1747970514685,-10.9441130877949));
#45483=CARTESIAN_POINT('Ctrl Pts',(8.89129495112497,-12.9729570348969,-9.31713358045354));
#45484=CARTESIAN_POINT('Ctrl Pts',(8.36752131451235,-14.5497923702765,-8.4003265416323));
#45485=CARTESIAN_POINT('Origin',(10.,0.,0.));
#45486=CARTESIAN_POINT('Origin',(7.68963026555328,-15.,8.16025403784512));
#45487=CARTESIAN_POINT('',(7.68963026555328,-15.,8.16025403784512));
#45488=CARTESIAN_POINT('',(7.6896302655531,-14.5669872981078,8.91025403784439));
#45489=CARTESIAN_POINT('',(7.6896302655531,-15.,8.16025403784439));
#45490=CARTESIAN_POINT('Ctrl Pts',(7.68963026555328,-15.,8.16025403784512));
#45491=CARTESIAN_POINT('Ctrl Pts',(7.80268870802714,-14.9249959521809,8.20015220863497));
#45492=CARTESIAN_POINT('Ctrl Pts',(7.91571517126633,-14.8499724569668,8.24010952390002));
#45493=CARTESIAN_POINT('Ctrl Pts',(8.14167814509372,-14.6999037370903,8.32013340767416));
#45494=CARTESIAN_POINT('Ctrl Pts',(8.2546169532586,-14.6248570018396,8.36020076335937));
#45495=CARTESIAN_POINT('Ctrl Pts',(8.36752131451236,-14.5497923702765,8.4003265416323));
#45496=CARTESIAN_POINT('Ctrl Pts',(8.36752131451235,-14.5497923702765,8.4003265416323));
#45497=CARTESIAN_POINT('Ctrl Pts',(8.25461606995072,-14.5525747644948,8.48539797417988));
#45498=CARTESIAN_POINT('Ctrl Pts',(8.14167637792964,-14.5553988066539,8.57042469607987));
#45499=CARTESIAN_POINT('Ctrl Pts',(7.91571340305211,-14.561130451635,8.74039996027625));
#45500=CARTESIAN_POINT('Ctrl Pts',(7.80268782367441,-14.5640381267354,8.8253502057819));
#45501=CARTESIAN_POINT('Ctrl Pts',(7.6896302655536,-14.5669872981074,8.91025403784458));
#45502=CARTESIAN_POINT('Origin',(8.36752131451236,5.55111512312578E-16,
16.8006530832646));
#45503=CARTESIAN_POINT('',(7.68963026555329,-0.433012701891581,17.0705080756891));
#45504=CARTESIAN_POINT('Ctrl Pts',(7.68963026555328,-0.433012701891577,
17.0705080756891));
#45505=CARTESIAN_POINT('Ctrl Pts',(7.80268870801826,-0.360957848519129,
17.0255017502896));
#45506=CARTESIAN_POINT('Ctrl Pts',(7.91571517126183,-0.288842050822766,
16.9805081551843));
#45507=CARTESIAN_POINT('Ctrl Pts',(8.14167814510512,-0.144504974616458,
16.8905567733386));
#45508=CARTESIAN_POINT('Ctrl Pts',(8.25461695326423,-0.072282259108921,
16.8455980719853));
#45509=CARTESIAN_POINT('Ctrl Pts',(8.36752131451235,4.44089209850063E-15,
16.8006530832646));
#45510=CARTESIAN_POINT('',(7.68963026555311,0.43301270189222,17.0705080756888));
#45511=CARTESIAN_POINT('Ctrl Pts',(8.36752131451236,1.66533453693773E-15,
16.8006530832646));
#45512=CARTESIAN_POINT('Ctrl Pts',(8.25461606995411,0.0722828246112067,
16.8455984236135));
#45513=CARTESIAN_POINT('Ctrl Pts',(8.14167637793691,0.144506104695097,16.8905574768131));
#45514=CARTESIAN_POINT('Ctrl Pts',(7.91571340304379,0.288843179023551,16.9805088590765));
#45515=CARTESIAN_POINT('Ctrl Pts',(7.80268782365699,0.360958412144736,17.0255021023359));
#45516=CARTESIAN_POINT('Ctrl Pts',(7.6896302655536,0.433012701892559,17.0705080756886));
#45517=CARTESIAN_POINT('',(7.68963026555311,-0.43301270189222,17.0705080756888));
#45518=CARTESIAN_POINT('Origin',(7.68963026555328,-14.5669872981084,-8.91025403784402));
#45519=CARTESIAN_POINT('',(7.68963026555328,-14.5669872981084,-8.91025403784402));
#45520=CARTESIAN_POINT('',(7.6896302655531,-15.,-8.16025403784439));
#45521=CARTESIAN_POINT('',(7.6896302655531,-14.5669872981078,-8.91025403784439));
#45522=CARTESIAN_POINT('Ctrl Pts',(7.68963026555328,-14.5669872981084,-8.91025403784402));
#45523=CARTESIAN_POINT('Ctrl Pts',(7.80268870801892,-14.5640381036676,-8.82534954165722));
#45524=CARTESIAN_POINT('Ctrl Pts',(7.91571517126228,-14.561130406147,-8.74039863128551));
#45525=CARTESIAN_POINT('Ctrl Pts',(8.14167814509705,-14.5553987624665,-8.57042336566644));
#45526=CARTESIAN_POINT('Ctrl Pts',(8.25461695326025,-14.552574742727,-8.4853973086269));
#45527=CARTESIAN_POINT('Ctrl Pts',(8.36752131451236,-14.5497923702765,-8.40032654163231));
#45528=CARTESIAN_POINT('Ctrl Pts',(8.36752131451236,-14.5497923702765,-8.4003265416323));
#45529=CARTESIAN_POINT('Ctrl Pts',(8.25461606994656,-14.624857589111,-8.36020044943344));
#45530=CARTESIAN_POINT('Ctrl Pts',(8.14167637792168,-14.6999049113589,-8.32013278073326));
#45531=CARTESIAN_POINT('Ctrl Pts',(7.91571340304811,-14.8499736306559,-8.24010889879555));
#45532=CARTESIAN_POINT('Ctrl Pts',(7.80268782366648,-14.9249965388743,-8.20015189654426));
#45533=CARTESIAN_POINT('Ctrl Pts',(7.6896302655536,-15.,-8.160254037844));
#45534=CARTESIAN_POINT('Origin',(8.36752131451236,14.5497923702765,8.4003265416323));
#45535=CARTESIAN_POINT('',(7.68963026555328,14.5669872981084,8.91025403784402));
#45536=CARTESIAN_POINT('Ctrl Pts',(7.68963026555328,14.5669872981084,8.91025403784401));
#45537=CARTESIAN_POINT('Ctrl Pts',(7.8026887080225,14.5640381036675,8.82534954165453));
#45538=CARTESIAN_POINT('Ctrl Pts',(7.91571517126384,14.561130406147,8.74039863128433));
#45539=CARTESIAN_POINT('Ctrl Pts',(8.14167814509868,14.5553987624664,8.5704233656652));
#45540=CARTESIAN_POINT('Ctrl Pts',(8.25461695326104,14.552574742727,8.4853973086263));
#45541=CARTESIAN_POINT('Ctrl Pts',(8.36752131451235,14.5497923702765,8.4003265416323));
#45542=CARTESIAN_POINT('',(7.68963026555311,15.,8.16025403784438));
#45543=CARTESIAN_POINT('Ctrl Pts',(8.36752131451236,14.5497923702765,8.40032654163229));
#45544=CARTESIAN_POINT('Ctrl Pts',(8.25461606994361,14.6248575891129,8.36020044943239));
#45545=CARTESIAN_POINT('Ctrl Pts',(8.14167637791574,14.6999049113629,8.32013278073115));
#45546=CARTESIAN_POINT('Ctrl Pts',(7.9157134030506,14.8499736306542,8.24010889879643));
#45547=CARTESIAN_POINT('Ctrl Pts',(7.8026878236717,14.9249965388709,8.20015189654609));
#45548=CARTESIAN_POINT('Ctrl Pts',(7.6896302655536,15.,8.16025403784399));
#45549=CARTESIAN_POINT('',(7.6896302655531,14.5669872981078,8.91025403784439));
#45550=CARTESIAN_POINT('Origin',(7.68963026555328,0.433012701891573,-17.0705080756891));
#45551=CARTESIAN_POINT('',(7.68963026555328,0.433012701891573,-17.0705080756891));
#45552=CARTESIAN_POINT('',(7.6896302655531,-0.433012701892221,-17.0705080756888));
#45553=CARTESIAN_POINT('',(7.68963026555311,0.433012701892215,-17.0705080756888));
#45554=CARTESIAN_POINT('Ctrl Pts',(7.68963026555328,0.433012701891573,-17.0705080756891));
#45555=CARTESIAN_POINT('Ctrl Pts',(7.8026887080221,0.360957848516674,-17.025501750288));
#45556=CARTESIAN_POINT('Ctrl Pts',(7.91571517126382,0.28884205082149,-16.9805081551835));
#45557=CARTESIAN_POINT('Ctrl Pts',(8.1416781451065,0.144504974615578,-16.890556773338));
#45558=CARTESIAN_POINT('Ctrl Pts',(8.25461695326464,0.0722822591086511,
-16.8455980719851));
#45559=CARTESIAN_POINT('Ctrl Pts',(8.36752131451235,-7.7715611723761E-15,
-16.8006530832646));
#45560=CARTESIAN_POINT('Ctrl Pts',(8.36752131451235,-4.44089209850063E-15,
-16.8006530832646));
#45561=CARTESIAN_POINT('Ctrl Pts',(8.25461606994312,-0.0722828246182448,
-16.8455984236178));
#45562=CARTESIAN_POINT('Ctrl Pts',(8.14167637791487,-0.144506104709167,
-16.8905574768218));
#45563=CARTESIAN_POINT('Ctrl Pts',(7.91571340305124,-0.288843179018781,
-16.9805088590736));
#45564=CARTESIAN_POINT('Ctrl Pts',(7.80268782367245,-0.360958412134893,
-17.0255021023297));
#45565=CARTESIAN_POINT('Ctrl Pts',(7.6896302655536,-0.433012701892566,-17.0705080756886));
#45566=CARTESIAN_POINT('Origin',(8.36752131451236,14.5497923702765,-8.40032654163231));
#45567=CARTESIAN_POINT('',(7.68963026555329,15.,-8.16025403784513));
#45568=CARTESIAN_POINT('Ctrl Pts',(7.68963026555329,15.,-8.16025403784513));
#45569=CARTESIAN_POINT('Ctrl Pts',(7.80268870802034,14.9249959521854,-8.20015220863258));
#45570=CARTESIAN_POINT('Ctrl Pts',(7.91571517126294,14.8499724569691,-8.24010952389882));
#45571=CARTESIAN_POINT('Ctrl Pts',(8.14167814509783,14.6999037370876,-8.32013340767562));
#45572=CARTESIAN_POINT('Ctrl Pts',(8.25461695326057,14.6248570018383,-8.36020076336009));
#45573=CARTESIAN_POINT('Ctrl Pts',(8.36752131451236,14.5497923702765,-8.40032654163231));
#45574=CARTESIAN_POINT('',(7.68963026555311,14.5669872981078,-8.91025403784439));
#45575=CARTESIAN_POINT('Ctrl Pts',(8.36752131451236,14.5497923702765,-8.40032654163231));
#45576=CARTESIAN_POINT('Ctrl Pts',(8.25461606994752,14.5525747644949,-8.4853979741823));
#45577=CARTESIAN_POINT('Ctrl Pts',(8.14167637792352,14.5553988066541,-8.57042469608449));
#45578=CARTESIAN_POINT('Ctrl Pts',(7.91571340305315,14.561130451635,-8.74039996027547));
#45579=CARTESIAN_POINT('Ctrl Pts',(7.80268782367616,14.5640381267354,-8.8253502057806));
#45580=CARTESIAN_POINT('Ctrl Pts',(7.6896302655536,14.5669872981074,-8.91025403784459));
#45581=CARTESIAN_POINT('',(7.68963026555311,15.,-8.16025403784439));
#45582=CARTESIAN_POINT('Ctrl Pts',(7.67668825215334,14.6070156607043,-8.88714365192406));
#45583=CARTESIAN_POINT('Ctrl Pts',(8.43313591503712,12.272413163364,-10.2350270322143));
#45584=CARTESIAN_POINT('Ctrl Pts',(9.03177916174122,9.05069193308572,-12.0950886517694));
#45585=CARTESIAN_POINT('Ctrl Pts',(8.82820572731108,4.69332251318476,-14.6108170593078));
#45586=CARTESIAN_POINT('Ctrl Pts',(8.18098669407586,1.94938600418923,-16.1950295414156));
#45587=CARTESIAN_POINT('Ctrl Pts',(7.67668825215334,0.392984339295657,-17.0936184616091));
#45588=CARTESIAN_POINT('Ctrl Pts',(7.90696593960635,14.5879412305617,-8.72487128182681));
#45589=CARTESIAN_POINT('Ctrl Pts',(8.67315119983517,12.2431218979784,-10.0818637214309));
#45590=CARTESIAN_POINT('Ctrl Pts',(9.28459893188896,8.99518638134712,-11.9614343524107));
#45591=CARTESIAN_POINT('Ctrl Pts',(9.07628688106433,4.59237548551847,-14.5017744624786));
#45592=CARTESIAN_POINT('Ctrl Pts',(8.41775611309223,1.82705595401861,-16.0945120758276));
#45593=CARTESIAN_POINT('Ctrl Pts',(7.90696593960635,0.261989559530435,-16.9959633354943));
#45594=CARTESIAN_POINT('Ctrl Pts',(8.13724362705935,14.5688668004191,-8.56259891172956));
#45595=CARTESIAN_POINT('Ctrl Pts',(8.91316648463323,12.2138306325927,-9.92870041064754));
#45596=CARTESIAN_POINT('Ctrl Pts',(9.5374187020367,8.93968082960853,-11.8277800530521));
#45597=CARTESIAN_POINT('Ctrl Pts',(9.32436803481757,4.49142845785217,-14.3927318656494));
#45598=CARTESIAN_POINT('Ctrl Pts',(8.6545255321086,1.70472590384799,-15.9939946102396));
#45599=CARTESIAN_POINT('Ctrl Pts',(8.13724362705935,0.130994779765213,-16.8983082093794));
#45600=CARTESIAN_POINT('Ctrl Pts',(8.36752131451236,14.5497923702765,-8.40032654163231));
#45601=CARTESIAN_POINT('Ctrl Pts',(9.15318176943128,12.1845393672071,-9.77553709986417));
#45602=CARTESIAN_POINT('Ctrl Pts',(9.79023847218445,8.88417527786995,-11.6941257536935));
#45603=CARTESIAN_POINT('Ctrl Pts',(9.57244918857082,4.39048143018587,-14.2836892688202));
#45604=CARTESIAN_POINT('Ctrl Pts',(8.89129495112497,1.58239585367736,-15.8934771446516));
#45605=CARTESIAN_POINT('Ctrl Pts',(8.36752131451235,-8.88178419700125E-15,
-16.8006530832646));
#45606=CARTESIAN_POINT('Ctrl Pts',(7.68963170841622,0.433013796132934,-17.0705074439286));
#45607=CARTESIAN_POINT('Ctrl Pts',(8.18653121623005,1.97292920995541,-16.1814368652289));
#45608=CARTESIAN_POINT('Ctrl Pts',(8.82870487706607,4.70400651959465,-14.6046486453311));
#45609=CARTESIAN_POINT('Ctrl Pts',(9.03128001198622,9.04000792667569,-12.1012570657462));
#45610=CARTESIAN_POINT('Ctrl Pts',(8.437237091211,12.2502959475146,-10.2477964127386));
#45611=CARTESIAN_POINT('Ctrl Pts',(7.68963261441509,14.5669848961069,-8.91025542464026));
#45612=CARTESIAN_POINT('Origin',(0.,14.7834936490539,-8.53525403784439));
#45613=CARTESIAN_POINT('',(0.,14.5669872981078,-8.91025403784439));
#45614=CARTESIAN_POINT('',(0.,15.,-8.16025403784439));
#45615=CARTESIAN_POINT('',(0.,14.7834936490539,-8.53525403784436));
#45616=CARTESIAN_POINT('',(0.,15.,-8.16025403784439));
#45617=CARTESIAN_POINT('',(0.,14.5669872981078,-8.91025403784439));
#45618=CARTESIAN_POINT('Ctrl Pts',(7.67668825215335,15.,8.20647480968506));
#45619=CARTESIAN_POINT('Ctrl Pts',(8.43313591503712,15.,5.5107080491046));
#45620=CARTESIAN_POINT('Ctrl Pts',(9.03209294028292,15.,1.79027110761766));
#45621=CARTESIAN_POINT('Ctrl Pts',(8.82833525724056,15.,-3.24081609633395));
#45622=CARTESIAN_POINT('Ctrl Pts',(8.18098669407586,15.,-6.4092969692981));
#45623=CARTESIAN_POINT('Ctrl Pts',(7.67668825215335,15.,-8.20647480968507));
#45624=CARTESIAN_POINT('Ctrl Pts',(7.90696593960635,14.8499307900922,8.27109205366748));
#45625=CARTESIAN_POINT('Ctrl Pts',(8.67315119983518,14.8527110492411,5.56192272456335));
#45626=CARTESIAN_POINT('Ctrl Pts',(9.2849107644129,14.856498377309,1.80901861973728));
#45627=CARTESIAN_POINT('Ctrl Pts',(9.07641678497459,14.8550928418347,-3.27371716647856));
#45628=CARTESIAN_POINT('Ctrl Pts',(8.41775611309223,14.8517842961914,-6.46497916759807));
#45629=CARTESIAN_POINT('Ctrl Pts',(7.90696593960635,14.8499307900922,-8.27109205366748));
#45630=CARTESIAN_POINT('Ctrl Pts',(8.13724362705935,14.6998615801843,8.33570929764989));
#45631=CARTESIAN_POINT('Ctrl Pts',(8.91316648463323,14.7054220984821,5.6131374000221));
#45632=CARTESIAN_POINT('Ctrl Pts',(9.53772858854289,14.7129967546181,1.82776613185691));
#45633=CARTESIAN_POINT('Ctrl Pts',(9.32449831270862,14.7101856836694,-3.30661823662315));
#45634=CARTESIAN_POINT('Ctrl Pts',(8.6545255321086,14.7035685923829,-6.52066136589804));
#45635=CARTESIAN_POINT('Ctrl Pts',(8.13724362705935,14.6998615801843,-8.3357092976499));
#45636=CARTESIAN_POINT('Ctrl Pts',(8.36752131451236,14.5497923702765,8.4003265416323));
#45637=CARTESIAN_POINT('Ctrl Pts',(9.15318176943128,14.5581331477232,5.66435207548085));
#45638=CARTESIAN_POINT('Ctrl Pts',(9.79054641267288,14.5694951319271,1.84651364397653));
#45639=CARTESIAN_POINT('Ctrl Pts',(9.57257984044265,14.565278525504,-3.33951930676775));
#45640=CARTESIAN_POINT('Ctrl Pts',(8.89129495112498,14.5553528885743,-6.57634356419801));
#45641=CARTESIAN_POINT('Ctrl Pts',(8.36752131451236,14.5497923702765,-8.40032654163231));
#45642=CARTESIAN_POINT('Ctrl Pts',(7.68963172268071,15.,-8.16025276820764));
#45643=CARTESIAN_POINT('Ctrl Pts',(8.18653232738211,15.,-6.38211114204574));
#45644=CARTESIAN_POINT('Ctrl Pts',(8.82883485876201,15.,-3.22848017464455));
#45645=CARTESIAN_POINT('Ctrl Pts',(9.03159333876146,15.,1.77793518592809));
#45646=CARTESIAN_POINT('Ctrl Pts',(8.43723924018764,15.,5.48516714116145));
#45647=CARTESIAN_POINT('Ctrl Pts',(7.68963263283691,15.,8.16025124584423));
#45648=CARTESIAN_POINT('Ctrl Pts',(7.67668825215334,-0.392984339295669,
-17.0936184616091));
#45649=CARTESIAN_POINT('Ctrl Pts',(8.43313591503712,-2.72758683663603,-15.7457350813189));
#45650=CARTESIAN_POINT('Ctrl Pts',(9.03177916174122,-5.94930806691429,-13.8856734617638));
#45651=CARTESIAN_POINT('Ctrl Pts',(8.82820572731108,-10.3066774868152,-11.3699450542253));
#45652=CARTESIAN_POINT('Ctrl Pts',(8.18098669407586,-13.0506139958108,-9.78573257211753));
#45653=CARTESIAN_POINT('Ctrl Pts',(7.67668825215334,-14.6070156607043,-8.88714365192405));
#45654=CARTESIAN_POINT('Ctrl Pts',(7.90696593960635,-0.261989559530447,
-16.9959633354943));
#45655=CARTESIAN_POINT('Ctrl Pts',(8.67315119983517,-2.60958915126271,-15.6437864459943));
#45656=CARTESIAN_POINT('Ctrl Pts',(9.28459893188896,-5.861312824214,-13.7707770942278));
#45657=CARTESIAN_POINT('Ctrl Pts',(9.07628688106433,-10.2627173416997,-11.2280010654152));
#45658=CARTESIAN_POINT('Ctrl Pts',(8.41775611309223,-13.0247283421728,-9.62953290822953));
#45659=CARTESIAN_POINT('Ctrl Pts',(7.90696593960635,-14.5879412305617,-8.7248712818268));
#45660=CARTESIAN_POINT('Ctrl Pts',(8.13724362705935,-0.130994779765225,
-16.8983082093794));
#45661=CARTESIAN_POINT('Ctrl Pts',(8.91316648463323,-2.49159146588939,-15.5418378106696));
#45662=CARTESIAN_POINT('Ctrl Pts',(9.5374187020367,-5.7733175815137,-13.6558807266918));
#45663=CARTESIAN_POINT('Ctrl Pts',(9.32436803481757,-10.2187571965841,-11.0860570766051));
#45664=CARTESIAN_POINT('Ctrl Pts',(8.6545255321086,-12.9988426885349,-9.47333324434154));
#45665=CARTESIAN_POINT('Ctrl Pts',(8.13724362705935,-14.5688668004191,-8.56259891172955));
#45666=CARTESIAN_POINT('Ctrl Pts',(8.36752131451236,-3.33066907387547E-15,
-16.8006530832646));
#45667=CARTESIAN_POINT('Ctrl Pts',(9.15318176943128,-2.37359378051606,-15.439889175345));
#45668=CARTESIAN_POINT('Ctrl Pts',(9.79023847218444,-5.6853223388134,-13.5409843591558));
#45669=CARTESIAN_POINT('Ctrl Pts',(9.57244918857082,-10.1747970514685,-10.9441130877949));
#45670=CARTESIAN_POINT('Ctrl Pts',(8.89129495112497,-12.9729570348969,-9.31713358045354));
#45671=CARTESIAN_POINT('Ctrl Pts',(8.36752131451235,-14.5497923702765,-8.4003265416323));
#45672=CARTESIAN_POINT('Ctrl Pts',(7.68963170841621,-14.5669862038671,-8.91025466960456));
#45673=CARTESIAN_POINT('Ctrl Pts',(8.18653121623004,-13.0270707900446,-9.79932524830422));
#45674=CARTESIAN_POINT('Ctrl Pts',(8.82870487706607,-10.2959934804053,-11.3761134682021));
#45675=CARTESIAN_POINT('Ctrl Pts',(9.03128001198622,-5.95999207332432,-13.8795050477869));
#45676=CARTESIAN_POINT('Ctrl Pts',(8.437237091211,-2.74970405248537,-15.7329657007945));
#45677=CARTESIAN_POINT('Ctrl Pts',(7.68963261441509,-0.433015103893123,
-17.0705066888929));
#45678=CARTESIAN_POINT('Origin',(0.,-3.01841884819964E-15,-17.0705080756888));
#45679=CARTESIAN_POINT('',(0.,-0.433012701892219,-17.0705080756888));
#45680=CARTESIAN_POINT('',(0.,0.433012701892215,-17.0705080756888));
#45681=CARTESIAN_POINT('',(0.,-2.33931761355391E-14,-17.0705080756888));
#45682=CARTESIAN_POINT('',(0.,0.433012701892215,-17.0705080756888));
#45683=CARTESIAN_POINT('',(0.,-0.433012701892221,-17.0705080756888));
#45684=CARTESIAN_POINT('Origin',(0.,14.7834936490539,8.53525403784439));
#45685=CARTESIAN_POINT('',(0.,15.,8.16025403784438));
#45686=CARTESIAN_POINT('',(0.,14.5669872981078,8.91025403784439));
#45687=CARTESIAN_POINT('',(0.,14.7834936490539,8.53525403784438));
#45688=CARTESIAN_POINT('',(0.,14.5669872981078,8.91025403784439));
#45689=CARTESIAN_POINT('',(0.,15.,8.16025403784438));
#45690=CARTESIAN_POINT('Ctrl Pts',(7.67668825215334,0.392984339295667,17.0936184616091));
#45691=CARTESIAN_POINT('Ctrl Pts',(8.43313591503712,2.72758683663604,15.7457350813189));
#45692=CARTESIAN_POINT('Ctrl Pts',(9.03177916174123,5.94930806691429,13.8856734617638));
#45693=CARTESIAN_POINT('Ctrl Pts',(8.82820572731109,10.3066774868152,11.3699450542253));
#45694=CARTESIAN_POINT('Ctrl Pts',(8.18098669407586,13.0506139958108,9.78573257211753));
#45695=CARTESIAN_POINT('Ctrl Pts',(7.67668825215334,14.6070156607043,8.88714365192404));
#45696=CARTESIAN_POINT('Ctrl Pts',(7.90696593960635,0.261989559530445,16.9959633354943));
#45697=CARTESIAN_POINT('Ctrl Pts',(8.67315119983518,2.60958915126271,15.6437864459943));
#45698=CARTESIAN_POINT('Ctrl Pts',(9.28459893188897,5.86131282421399,13.7707770942278));
#45699=CARTESIAN_POINT('Ctrl Pts',(9.07628688106433,10.2627173416997,11.2280010654152));
#45700=CARTESIAN_POINT('Ctrl Pts',(8.41775611309223,13.0247283421728,9.62953290822953));
#45701=CARTESIAN_POINT('Ctrl Pts',(7.90696593960635,14.5879412305617,8.72487128182679));
#45702=CARTESIAN_POINT('Ctrl Pts',(8.13724362705935,0.130994779765222,16.8983082093794));
#45703=CARTESIAN_POINT('Ctrl Pts',(8.91316648463323,2.49159146588939,15.5418378106696));
#45704=CARTESIAN_POINT('Ctrl Pts',(9.53741870203671,5.7733175815137,13.6558807266918));
#45705=CARTESIAN_POINT('Ctrl Pts',(9.32436803481758,10.2187571965841,11.0860570766051));
#45706=CARTESIAN_POINT('Ctrl Pts',(8.6545255321086,12.9988426885349,9.47333324434154));
#45707=CARTESIAN_POINT('Ctrl Pts',(8.13724362705935,14.5688668004191,8.56259891172954));
#45708=CARTESIAN_POINT('Ctrl Pts',(8.36752131451236,-5.55111512312578E-16,
16.8006530832646));
#45709=CARTESIAN_POINT('Ctrl Pts',(9.15318176943128,2.37359378051606,15.439889175345));
#45710=CARTESIAN_POINT('Ctrl Pts',(9.79023847218445,5.68532233881341,13.5409843591558));
#45711=CARTESIAN_POINT('Ctrl Pts',(9.57244918857082,10.1747970514685,10.9441130877949));
#45712=CARTESIAN_POINT('Ctrl Pts',(8.89129495112497,12.9729570348969,9.31713358045354));
#45713=CARTESIAN_POINT('Ctrl Pts',(8.36752131451235,14.5497923702765,8.4003265416323));
#45714=CARTESIAN_POINT('Ctrl Pts',(7.68963170841621,14.5669862038671,8.91025466960456));
#45715=CARTESIAN_POINT('Ctrl Pts',(8.18653121623005,13.0270707900446,9.79932524830422));
#45716=CARTESIAN_POINT('Ctrl Pts',(8.82870487706607,10.2959934804054,11.3761134682021));
#45717=CARTESIAN_POINT('Ctrl Pts',(9.03128001198623,5.95999207332431,13.8795050477869));
#45718=CARTESIAN_POINT('Ctrl Pts',(8.43723709121101,2.74970405248537,15.7329657007945));
#45719=CARTESIAN_POINT('Ctrl Pts',(7.68963261441509,0.43301510389312,17.0705066888929));
#45720=CARTESIAN_POINT('Ctrl Pts',(7.67668825215334,-15.,-8.20647480968506));
#45721=CARTESIAN_POINT('Ctrl Pts',(8.43313591503712,-15.,-5.5107080491046));
#45722=CARTESIAN_POINT('Ctrl Pts',(9.03209294028291,-15.,-1.79027110761766));
#45723=CARTESIAN_POINT('Ctrl Pts',(8.82833525724056,-15.,3.24081609633395));
#45724=CARTESIAN_POINT('Ctrl Pts',(8.18098669407586,-15.,6.40929696929809));
#45725=CARTESIAN_POINT('Ctrl Pts',(7.67668825215334,-15.,8.20647480968506));
#45726=CARTESIAN_POINT('Ctrl Pts',(7.90696593960635,-14.8499307900922,-8.27109205366748));
#45727=CARTESIAN_POINT('Ctrl Pts',(8.67315119983517,-14.8527110492411,-5.56192272456335));
#45728=CARTESIAN_POINT('Ctrl Pts',(9.2849107644129,-14.856498377309,-1.80901861973728));
#45729=CARTESIAN_POINT('Ctrl Pts',(9.07641678497459,-14.8550928418347,3.27371716647854));
#45730=CARTESIAN_POINT('Ctrl Pts',(8.41775611309223,-14.8517842961914,6.46497916759806));
#45731=CARTESIAN_POINT('Ctrl Pts',(7.90696593960635,-14.8499307900922,8.27109205366747));
#45732=CARTESIAN_POINT('Ctrl Pts',(8.13724362705935,-14.6998615801843,-8.33570929764989));
#45733=CARTESIAN_POINT('Ctrl Pts',(8.91316648463323,-14.7054220984821,-5.6131374000221));
#45734=CARTESIAN_POINT('Ctrl Pts',(9.53772858854288,-14.7129967546181,-1.82776613185692));
#45735=CARTESIAN_POINT('Ctrl Pts',(9.32449831270862,-14.7101856836694,3.30661823662315));
#45736=CARTESIAN_POINT('Ctrl Pts',(8.6545255321086,-14.7035685923829,6.52066136589803));
#45737=CARTESIAN_POINT('Ctrl Pts',(8.13724362705935,-14.6998615801843,8.33570929764989));
#45738=CARTESIAN_POINT('Ctrl Pts',(8.36752131451236,-14.5497923702765,-8.4003265416323));
#45739=CARTESIAN_POINT('Ctrl Pts',(9.15318176943128,-14.5581331477232,-5.66435207548086));
#45740=CARTESIAN_POINT('Ctrl Pts',(9.79054641267287,-14.5694951319271,-1.84651364397654));
#45741=CARTESIAN_POINT('Ctrl Pts',(9.57257984044265,-14.5652785255041,3.33951930676774));
#45742=CARTESIAN_POINT('Ctrl Pts',(8.89129495112497,-14.5553528885743,6.576343564198));
#45743=CARTESIAN_POINT('Ctrl Pts',(8.36752131451236,-14.5497923702765,8.4003265416323));
#45744=CARTESIAN_POINT('Ctrl Pts',(7.6896317226807,-15.,8.16025276820764));
#45745=CARTESIAN_POINT('Ctrl Pts',(8.1865323273821,-15.,6.38211114204573));
#45746=CARTESIAN_POINT('Ctrl Pts',(8.828834858762,-15.,3.22848017464454));
#45747=CARTESIAN_POINT('Ctrl Pts',(9.03159333876145,-15.,-1.77793518592809));
#45748=CARTESIAN_POINT('Ctrl Pts',(8.43723924018764,-15.,-5.48516714116146));
#45749=CARTESIAN_POINT('Ctrl Pts',(7.68963263283691,-15.,-8.16025124584424));
#45750=CARTESIAN_POINT('Origin',(0.,-14.7834936490539,-8.53525403784439));
#45751=CARTESIAN_POINT('',(0.,-15.,-8.16025403784439));
#45752=CARTESIAN_POINT('',(0.,-14.5669872981078,-8.91025403784439));
#45753=CARTESIAN_POINT('',(0.,-14.7834936490539,-8.53525403784438));
#45754=CARTESIAN_POINT('',(0.,-14.5669872981078,-8.91025403784439));
#45755=CARTESIAN_POINT('',(0.,-15.,-8.16025403784439));
#45756=CARTESIAN_POINT('Origin',(0.,4.16333634234434E-16,17.0705080756888));
#45757=CARTESIAN_POINT('',(0.,0.433012701892219,17.0705080756888));
#45758=CARTESIAN_POINT('',(0.,-0.43301270189222,17.0705080756888));
#45759=CARTESIAN_POINT('',(0.,-2.1675799894322E-14,17.0705080756888));
#45760=CARTESIAN_POINT('',(0.,-0.43301270189222,17.0705080756888));
#45761=CARTESIAN_POINT('',(0.,0.43301270189222,17.0705080756888));
#45762=CARTESIAN_POINT('Ctrl Pts',(7.67668825215334,-14.6070156607043,8.88714365192404));
#45763=CARTESIAN_POINT('Ctrl Pts',(8.43313591503712,-12.272413163364,10.2350270322143));
#45764=CARTESIAN_POINT('Ctrl Pts',(9.03177916174123,-9.05069193308572,12.0950886517694));
#45765=CARTESIAN_POINT('Ctrl Pts',(8.82820572731109,-4.69332251318478,14.6108170593078));
#45766=CARTESIAN_POINT('Ctrl Pts',(8.18098669407586,-1.94938600418924,16.1950295414156));
#45767=CARTESIAN_POINT('Ctrl Pts',(7.67668825215334,-0.392984339295662,
17.0936184616091));
#45768=CARTESIAN_POINT('Ctrl Pts',(7.90696593960635,-14.5879412305617,8.7248712818268));
#45769=CARTESIAN_POINT('Ctrl Pts',(8.67315119983517,-12.2431218979784,10.0818637214309));
#45770=CARTESIAN_POINT('Ctrl Pts',(9.28459893188897,-8.99518638134712,11.9614343524107));
#45771=CARTESIAN_POINT('Ctrl Pts',(9.07628688106433,-4.59237548551848,14.5017744624786));
#45772=CARTESIAN_POINT('Ctrl Pts',(8.41775611309223,-1.82705595401862,16.0945120758276));
#45773=CARTESIAN_POINT('Ctrl Pts',(7.90696593960635,-0.26198955953044,16.9959633354943));
#45774=CARTESIAN_POINT('Ctrl Pts',(8.13724362705935,-14.5688668004191,8.56259891172955));
#45775=CARTESIAN_POINT('Ctrl Pts',(8.91316648463323,-12.2138306325927,9.92870041064753));
#45776=CARTESIAN_POINT('Ctrl Pts',(9.53741870203671,-8.93968082960854,11.8277800530521));
#45777=CARTESIAN_POINT('Ctrl Pts',(9.32436803481758,-4.49142845785218,14.3927318656494));
#45778=CARTESIAN_POINT('Ctrl Pts',(8.6545255321086,-1.704725903848,15.9939946102396));
#45779=CARTESIAN_POINT('Ctrl Pts',(8.13724362705935,-0.130994779765218,
16.8983082093794));
#45780=CARTESIAN_POINT('Ctrl Pts',(8.36752131451235,-14.5497923702765,8.4003265416323));
#45781=CARTESIAN_POINT('Ctrl Pts',(9.15318176943129,-12.1845393672071,9.77553709986416));
#45782=CARTESIAN_POINT('Ctrl Pts',(9.79023847218445,-8.88417527786995,11.6941257536935));
#45783=CARTESIAN_POINT('Ctrl Pts',(9.57244918857083,-4.39048143018589,14.2836892688202));
#45784=CARTESIAN_POINT('Ctrl Pts',(8.89129495112497,-1.58239585367737,15.8934771446515));
#45785=CARTESIAN_POINT('Ctrl Pts',(8.36752131451235,4.44089209850063E-15,
16.8006530832646));
#45786=CARTESIAN_POINT('Ctrl Pts',(7.68963170841622,-0.433013796132936,
17.0705074439286));
#45787=CARTESIAN_POINT('Ctrl Pts',(8.18653121623005,-1.97292920995542,16.1814368652289));
#45788=CARTESIAN_POINT('Ctrl Pts',(8.82870487706608,-4.70400651959466,14.604648645331));
#45789=CARTESIAN_POINT('Ctrl Pts',(9.03128001198623,-9.04000792667568,12.1012570657462));
#45790=CARTESIAN_POINT('Ctrl Pts',(8.437237091211,-12.2502959475146,10.2477964127386));
#45791=CARTESIAN_POINT('Ctrl Pts',(7.68963261441509,-14.5669848961069,8.91025542464025));
#45792=CARTESIAN_POINT('Origin',(0.,-14.7834936490539,8.53525403784439));
#45793=CARTESIAN_POINT('',(0.,-14.5669872981078,8.91025403784439));
#45794=CARTESIAN_POINT('',(0.,-15.,8.16025403784439));
#45795=CARTESIAN_POINT('',(0.,-14.7834936490539,8.5352540378444));
#45796=CARTESIAN_POINT('',(0.,-15.,8.16025403784439));
#45797=CARTESIAN_POINT('',(0.,-14.5669872981078,8.91025403784439));
#45798=CARTESIAN_POINT('Origin',(0.,0.,0.));
#45799=CARTESIAN_POINT('',(1.11022302462516E-15,-1.14252408577115,-16.6608714872132));
#45800=CARTESIAN_POINT('',(0.,-15.,-8.66025403784439));
#45801=CARTESIAN_POINT('',(1.11022302462516E-15,1.14252408577115,-16.6608714872132));
#45802=CARTESIAN_POINT('Origin',(0.,0.,0.));
#45803=CARTESIAN_POINT('',(0.,-3.18172571617472E-15,-17.3205080756888));
#45804=CARTESIAN_POINT('Origin',(0.,-15.,-8.66025403784439));
#45805=CARTESIAN_POINT('',(1.11022302462516E-15,-13.8574759142288,-9.31989062632));
#45806=CARTESIAN_POINT('',(0.,-15.,-8.66025403784439));
#45807=CARTESIAN_POINT('',(0.,-11.25,-10.8253175473055));
#45808=CARTESIAN_POINT('Origin',(0.,0.,0.));
#45809=CARTESIAN_POINT('',(1.11022302462516E-15,-15.,-7.34098086089318));
#45810=CARTESIAN_POINT('',(0.,-15.,8.66025403784439));
#45811=CARTESIAN_POINT('Origin',(0.,0.,0.));
#45812=CARTESIAN_POINT('Origin',(0.,-15.,8.66025403784439));
#45813=CARTESIAN_POINT('',(1.11022302462516E-15,-15.,7.34098086089317));
#45814=CARTESIAN_POINT('',(0.,-15.,8.66025403784439));
#45815=CARTESIAN_POINT('',(0.,-15.,4.33012701892219));
#45816=CARTESIAN_POINT('Origin',(0.,0.,0.));
#45817=CARTESIAN_POINT('',(1.11022302462516E-15,-13.8574759142288,9.31989062631999));
#45818=CARTESIAN_POINT('',(0.,1.06057523872491E-15,17.3205080756888));
#45819=CARTESIAN_POINT('Origin',(0.,0.,0.));
#45820=CARTESIAN_POINT('Origin',(0.,1.06057523872491E-15,17.3205080756888));
#45821=CARTESIAN_POINT('',(1.11022302462516E-15,-1.14252408577115,16.6608714872132));
#45822=CARTESIAN_POINT('',(0.,1.06057523872491E-15,17.3205080756888));
#45823=CARTESIAN_POINT('',(0.,-3.75,15.1554445662277));
#45824=CARTESIAN_POINT('Origin',(0.,15.,8.66025403784439));
#45825=CARTESIAN_POINT('',(1.11022302462516E-15,13.8574759142288,9.31989062631999));
#45826=CARTESIAN_POINT('',(0.,15.,8.66025403784439));
#45827=CARTESIAN_POINT('',(1.11022302462516E-15,1.14252408577115,16.6608714872132));
#45828=CARTESIAN_POINT('',(0.,11.25,10.8253175473055));
#45829=CARTESIAN_POINT('',(0.,15.,8.66025403784439));
#45830=CARTESIAN_POINT('Origin',(0.,15.,-8.66025403784439));
#45831=CARTESIAN_POINT('',(1.11022302462516E-15,15.,-7.34098086089319));
#45832=CARTESIAN_POINT('',(0.,15.,-8.66025403784439));
#45833=CARTESIAN_POINT('',(1.11022302462516E-15,15.,7.34098086089318));
#45834=CARTESIAN_POINT('',(0.,15.,-4.3301270189222));
#45835=CARTESIAN_POINT('',(0.,15.,-8.66025403784439));
#45836=CARTESIAN_POINT('Origin',(0.,0.,0.));
#45837=CARTESIAN_POINT('',(1.11022302462516E-15,13.8574759142288,-9.31989062632));
#45838=CARTESIAN_POINT('',(0.,-3.18172571617472E-15,-17.3205080756888));
#45839=CARTESIAN_POINT('Origin',(0.,0.,0.));
#45840=CARTESIAN_POINT('Origin',(0.,0.,0.));
#45841=CARTESIAN_POINT('Origin',(0.,0.,0.));
#45842=CARTESIAN_POINT('Origin',(0.,0.,0.));
#45843=CARTESIAN_POINT('Origin',(0.,0.,0.));
#45844=CARTESIAN_POINT('Origin',(0.,-3.18172571617472E-15,-17.3205080756888));
#45845=CARTESIAN_POINT('',(0.,3.75,-15.1554445662277));
#45846=CARTESIAN_POINT('Origin',(0.,0.,0.));
#45847=CARTESIAN_POINT('Origin',(0.,0.,0.));
#45848=CARTESIAN_POINT('Origin',(0.,0.,0.));
#45849=CARTESIAN_POINT('Origin',(0.,0.,0.));
#45850=CARTESIAN_POINT('Origin',(0.,0.,0.));
#45851=CARTESIAN_POINT('Origin',(0.,0.,0.));
#45852=CARTESIAN_POINT('Origin',(0.,0.,0.));
#45853=CARTESIAN_POINT('Origin',(0.,0.,0.));
#45854=CARTESIAN_POINT('Origin',(0.,0.,0.));
#45855=CARTESIAN_POINT('Origin',(0.,0.,0.));
#45856=CARTESIAN_POINT('Origin',(0.,0.,0.));
#45857=CARTESIAN_POINT('',(1.11022302462516E-15,-16.7,-2.04516015457608E-15));
#45858=CARTESIAN_POINT('Origin',(0.,0.,0.));
#45859=CARTESIAN_POINT('Origin',(0.,0.,0.));
#45860=CARTESIAN_POINT('Origin',(-18.,16.2,0.));
#45861=CARTESIAN_POINT('',(-18.,-16.2,-1.98392781461871E-15));
#45862=CARTESIAN_POINT('Origin',(-18.,0.,0.));
#45863=CARTESIAN_POINT('Origin',(-17.75,0.,0.));
#45864=CARTESIAN_POINT('',(-17.5,-16.7,-2.04516015457608E-15));
#45865=CARTESIAN_POINT('Origin',(-17.5,0.,0.));
#45866=CARTESIAN_POINT('',(-17.75,-16.45,-2.0145439845974E-15));
#45867=CARTESIAN_POINT('Origin',(-8.75,0.,0.));
#45868=CARTESIAN_POINT('',(-8.75,-16.7,-2.04516015457608E-15));
#55708=UNCERTAINTY_MEASURE_WITH_UNIT(LENGTH_MEASURE(0.01),#55738,
'DISTANCE_ACCURACY_VALUE',
'Maximum model space distance between geometric entities at asserted c
onnectivities');
#55715=UNCERTAINTY_MEASURE_WITH_UNIT(LENGTH_MEASURE(0.01),#55738,
'DISTANCE_ACCURACY_VALUE',
'Maximum model space distance between geometric entities at asserted c
onnectivities');
#55730=(
GEOMETRIC_REPRESENTATION_CONTEXT(3)
GLOBAL_UNCERTAINTY_ASSIGNED_CONTEXT((#55708))
GLOBAL_UNIT_ASSIGNED_CONTEXT((#55738,#55740,#55741))
REPRESENTATION_CONTEXT('','3D')
);
#55737=(
GEOMETRIC_REPRESENTATION_CONTEXT(3)
GLOBAL_UNCERTAINTY_ASSIGNED_CONTEXT((#55715))
GLOBAL_UNIT_ASSIGNED_CONTEXT((#55738,#55740,#55741))
REPRESENTATION_CONTEXT('','3D')
);
#55738=(
LENGTH_UNIT()
NAMED_UNIT(*)
SI_UNIT(.MILLI.,.METRE.)
);
#55740=(
NAMED_UNIT(*)
PLANE_ANGLE_UNIT()
SI_UNIT($,.RADIAN.)
);
#55741=(
NAMED_UNIT(*)
SI_UNIT($,.STERADIAN.)
SOLID_ANGLE_UNIT()
);
#55756=SHAPE_DEFINITION_REPRESENTATION(#55777,#55834);
#55777=PRODUCT_DEFINITION_SHAPE('',$,#55856);
#55834=SHAPE_REPRESENTATION('',(#29252),#55730);
#55841=PRODUCT_DEFINITION_CONTEXT('part definition',#55906,'design');
#55856=PRODUCT_DEFINITION('2026-10-26-00-34-32-795',
'16_Port_Plug_1in_NPT',#55877,#55841);
#55877=PRODUCT_DEFINITION_FORMATION('',$,#55922);
#55906=APPLICATION_CONTEXT(
'Core Data for Automotive Mechanical Design Process');
#55907=PRODUCT_CONTEXT('part definition',#55906,'mechanical');
#55922=PRODUCT('2026-10-26-00-34-32-795','16_Port_Plug_1in_NPT',$,(#55907));
#55971=COLOUR_RGB('Light Blue',0.38,0.62,0.78);
#55972=FILL_AREA_STYLE_COLOUR('',#55971);
#55973=FILL_AREA_STYLE('',(#55972));
#55974=SURFACE_STYLE_FILL_AREA(#55973);
#55975=SURFACE_SIDE_STYLE('',(#55974));
#55976=SURFACE_STYLE_USAGE(.BOTH.,#55975);
#55977=PRESENTATION_STYLE_ASSIGNMENT((#55976));
ENDSEC;
END-ISO-10303-21;
